ISO-10303-21;
HEADER;
/* Generated by software containing ST-Developer
 * from STEP Tools, Inc. (www.steptools.com) 
 */

FILE_DESCRIPTION(
/* description */ (''),
/* implementation_level */ '2;1');

FILE_NAME(
/* name */ 'Top_Block.step',
/* time_stamp */ '2026-10-23T17:00:58+06:00',
/* author */ (''),
/* organization */ (''),
/* preprocessor_version */ 'ST-DEVELOPER v20.2',
/* originating_system */ 'Autodesk Translation Framework v15.15.0.0',
/* authorisation */ '');

FILE_SCHEMA (('AUTOMOTIVE_DESIGN { 1 0 10303 214 3 1 1 }'));
ENDSEC;

DATA;
#10=MECHANICAL_DESIGN_GEOMETRIC_PRESENTATION_REPRESENTATION('',(#106),#11385);
#80=SHAPE_REPRESENTATION_RELATIONSHIP('SRR','None',#11432,#93);
#93=ADVANCED_BREP_SHAPE_REPRESENTATION('',(#119),#11372);
#106=STYLED_ITEM('',(#11546),#119);
#119=MANIFOLD_SOLID_BREP('Top_Block',#5342);
#132=FACE_BOUND('',#1018,.T.);
#133=FACE_BOUND('',#1019,.T.);
#134=FACE_BOUND('',#1020,.T.);
#135=FACE_BOUND('',#1021,.T.);
#136=FACE_BOUND('',#1022,.T.);
#137=FACE_BOUND('',#1023,.T.);
#138=FACE_BOUND('',#1024,.T.);
#139=FACE_BOUND('',#1077,.T.);
#140=FACE_BOUND('',#1078,.T.);
#141=FACE_BOUND('',#1079,.T.);
#142=FACE_BOUND('',#1080,.T.);
#143=FACE_BOUND('',#1081,.T.);
#144=FACE_BOUND('',#1082,.T.);
#145=FACE_BOUND('',#1083,.T.);
#146=FACE_BOUND('',#1085,.T.);
#147=FACE_BOUND('',#1087,.T.);
#148=FACE_BOUND('',#1089,.T.);
#149=FACE_BOUND('',#1091,.T.);
#173=B_SPLINE_CURVE_WITH_KNOTS('',3,(#8003,#8004,#8005,#8006,#8007,#8008,
#8009,#8010,#8011,#8012),.UNSPECIFIED.,.F.,.F.,(4,2,2,2,4),(0.,0.0304288686048288,
0.0608577372096576,0.0912866058144864,0.121715474419315),.UNSPECIFIED.);
#174=B_SPLINE_CURVE_WITH_KNOTS('',3,(#8306,#8307,#8308,#8309,#8310,#8311,
#8312,#8313,#8314,#8315),.UNSPECIFIED.,.F.,.F.,(4,2,2,2,4),(0.,0.0304288686048287,
0.0608577372096575,0.0912866058144862,0.121715474419315),.UNSPECIFIED.);
#183=CONICAL_SURFACE('',#5571,5.8095085413358,0.785398163397448);
#184=CONICAL_SURFACE('',#5574,99.75,0.785398163397445);
#185=CONICAL_SURFACE('',#5578,1.25000000000098,0.785398163397449);
#186=CONICAL_SURFACE('',#5582,0.750000000000013,0.785398163397449);
#187=CONICAL_SURFACE('',#5586,0.750000000000014,0.785398163397448);
#188=CONICAL_SURFACE('',#5590,0.749999999999996,0.785398163397449);
#189=CONICAL_SURFACE('',#5594,0.750000000000022,0.785398163397448);
#190=CONICAL_SURFACE('',#5598,1.25000000000025,0.785398163397447);
#191=CONICAL_SURFACE('',#5602,1.25000000000039,0.785398163397448);
#192=CONICAL_SURFACE('',#5606,4.05072977423739,0.785398163397448);
#193=CONICAL_SURFACE('',#5610,1.25000000000039,0.785398163397448);
#194=CONICAL_SURFACE('',#5614,1.25000000000025,0.785398163397447);
#195=CONICAL_SURFACE('',#5618,0.750000000000022,0.785398163397448);
#196=CONICAL_SURFACE('',#5622,0.749999999999996,0.785398163397449);
#197=CONICAL_SURFACE('',#5626,0.750000000000014,0.785398163397448);
#198=CONICAL_SURFACE('',#5630,0.750000000000013,0.785398163397449);
#199=CONICAL_SURFACE('',#5634,1.25000000000098,0.785398163397449);
#200=CONICAL_SURFACE('',#5638,99.75,0.785398163397445);
#201=CONICAL_SURFACE('',#5641,5.8095085413358,0.785398163397447);
#202=CONICAL_SURFACE('',#5678,5.8095085413358,0.785398163397448);
#203=CONICAL_SURFACE('',#5680,99.75,0.785398163397446);
#204=CONICAL_SURFACE('',#5683,1.25000000000098,0.78539816339745);
#205=CONICAL_SURFACE('',#5686,0.750000000000013,0.785398163397449);
#206=CONICAL_SURFACE('',#5689,0.750000000000014,0.785398163397449);
#207=CONICAL_SURFACE('',#5692,0.749999999999996,0.785398163397449);
#208=CONICAL_SURFACE('',#5695,0.750000000000022,0.785398163397448);
#209=CONICAL_SURFACE('',#5698,1.25000000000025,0.785398163397448);
#210=CONICAL_SURFACE('',#5701,1.25000000000039,0.785398163397448);
#211=CONICAL_SURFACE('',#5704,4.05072977423739,0.785398163397448);
#212=CONICAL_SURFACE('',#5708,1.25000000000039,0.785398163397448);
#213=CONICAL_SURFACE('',#5712,1.25000000000025,0.785398163397448);
#214=CONICAL_SURFACE('',#5716,0.750000000000022,0.785398163397449);
#215=CONICAL_SURFACE('',#5720,0.749999999999996,0.785398163397449);
#216=CONICAL_SURFACE('',#5724,0.750000000000014,0.785398163397448);
#217=CONICAL_SURFACE('',#5728,0.750000000000013,0.78539816339745);
#218=CONICAL_SURFACE('',#5732,1.25000000000098,0.78539816339745);
#219=CONICAL_SURFACE('',#5736,99.75,0.785398163397446);
#220=CONICAL_SURFACE('',#5739,5.8095085413358,0.785398163397449);
#221=CONICAL_SURFACE('',#5767,3.40761552865316,0.785398163397446);
#222=CONICAL_SURFACE('',#5770,3.40761552865316,0.785398163397448);
#223=CONICAL_SURFACE('',#5773,3.40761552865316,0.785398163397446);
#273=CIRCLE('',#5503,1.97957176368631);
#274=CIRCLE('',#5504,1.97957176368631);
#275=CIRCLE('',#5507,1.45);
#276=CIRCLE('',#5508,1.45);
#277=CIRCLE('',#5511,1.97957176368631);
#278=CIRCLE('',#5512,1.97957176368631);
#279=CIRCLE('',#5515,1.45);
#280=CIRCLE('',#5516,1.45);
#281=CIRCLE('',#5519,1.97957176368631);
#282=CIRCLE('',#5520,1.97957176368631);
#283=CIRCLE('',#5523,1.45);
#284=CIRCLE('',#5524,1.45);
#285=CIRCLE('',#5527,1.97957176368631);
#286=CIRCLE('',#5528,1.97957176368631);
#287=CIRCLE('',#5531,1.45);
#288=CIRCLE('',#5532,1.45);
#289=CIRCLE('',#5535,1.45);
#290=CIRCLE('',#5536,1.45);
#291=CIRCLE('',#5539,1.97957176368631);
#292=CIRCLE('',#5540,1.97957176368631);
#293=CIRCLE('',#5543,1.45);
#294=CIRCLE('',#5544,1.45);
#295=CIRCLE('',#5547,1.97957176368631);
#296=CIRCLE('',#5548,1.97957176368631);
#297=CIRCLE('',#5551,1.97957176368631);
#298=CIRCLE('',#5552,1.97957176368631);
#299=CIRCLE('',#5555,1.45);
#300=CIRCLE('',#5556,1.45);
#301=CIRCLE('',#5559,1.97957176368631);
#302=CIRCLE('',#5560,1.97957176368631);
#303=CIRCLE('',#5563,1.45);
#304=CIRCLE('',#5564,1.45);
#305=CIRCLE('',#5566,1.77957176368631);
#306=CIRCLE('',#5567,1.77957176368631);
#307=CIRCLE('',#5569,1.77957176368631);
#308=CIRCLE('',#5570,1.77957176368631);
#309=CIRCLE('',#5572,6.0595085413358);
#310=CIRCLE('',#5573,5.5595085413358);
#311=CIRCLE('',#5575,100.);
#312=CIRCLE('',#5576,99.5);
#313=CIRCLE('',#5579,1.50000000000098);
#314=CIRCLE('',#5580,1.00000000000098);
#315=CIRCLE('',#5583,1.00000000000001);
#316=CIRCLE('',#5584,0.500000000000012);
#317=CIRCLE('',#5587,1.00000000000001);
#318=CIRCLE('',#5588,0.500000000000014);
#319=CIRCLE('',#5591,0.999999999999996);
#320=CIRCLE('',#5592,0.499999999999995);
#321=CIRCLE('',#5595,1.00000000000002);
#322=CIRCLE('',#5596,0.500000000000022);
#323=CIRCLE('',#5599,1.50000000000025);
#324=CIRCLE('',#5600,1.00000000000025);
#325=CIRCLE('',#5603,1.50000000000039);
#326=CIRCLE('',#5604,1.00000000000039);
#327=CIRCLE('',#5607,3.80072977423739);
#328=CIRCLE('',#5608,4.30072977423739);
#329=CIRCLE('',#5611,1.00000000000039);
#330=CIRCLE('',#5612,1.50000000000039);
#331=CIRCLE('',#5615,1.00000000000025);
#332=CIRCLE('',#5616,1.50000000000025);
#333=CIRCLE('',#5619,0.500000000000022);
#334=CIRCLE('',#5620,1.00000000000002);
#335=CIRCLE('',#5623,0.499999999999995);
#336=CIRCLE('',#5624,0.999999999999996);
#337=CIRCLE('',#5627,0.500000000000014);
#338=CIRCLE('',#5628,1.00000000000001);
#339=CIRCLE('',#5631,0.500000000000012);
#340=CIRCLE('',#5632,1.00000000000001);
#341=CIRCLE('',#5635,1.00000000000098);
#342=CIRCLE('',#5636,1.50000000000098);
#343=CIRCLE('',#5639,100.);
#344=CIRCLE('',#5640,99.5);
#345=CIRCLE('',#5642,5.5595085413358);
#346=CIRCLE('',#5643,6.0595085413358);
#347=CIRCLE('',#5646,1.50000000000039);
#348=CIRCLE('',#5649,1.50000000000025);
#349=CIRCLE('',#5652,1.00000000000002);
#350=CIRCLE('',#5655,0.999999999999996);
#351=CIRCLE('',#5658,1.00000000000001);
#352=CIRCLE('',#5661,1.00000000000001);
#353=CIRCLE('',#5664,1.50000000000098);
#354=CIRCLE('',#5667,100.);
#355=CIRCLE('',#5669,5.5595085413358);
#356=CIRCLE('',#5671,5.5595085413358);
#357=CIRCLE('',#5673,3.65761552865316);
#358=CIRCLE('',#5674,3.65761552865316);
#359=CIRCLE('',#5675,1.77957176368631);
#360=CIRCLE('',#5676,1.77957176368631);
#361=CIRCLE('',#5677,3.65761552865316);
#362=CIRCLE('',#5679,6.0595085413358);
#363=CIRCLE('',#5681,99.5);
#364=CIRCLE('',#5684,1.00000000000098);
#365=CIRCLE('',#5687,0.500000000000012);
#366=CIRCLE('',#5690,0.500000000000014);
#367=CIRCLE('',#5693,0.499999999999995);
#368=CIRCLE('',#5696,0.500000000000022);
#369=CIRCLE('',#5699,1.00000000000025);
#370=CIRCLE('',#5702,1.00000000000039);
#371=CIRCLE('',#5705,4.30072977423739);
#372=CIRCLE('',#5706,3.80072977423739);
#373=CIRCLE('',#5709,1.00000000000039);
#374=CIRCLE('',#5710,1.50000000000039);
#375=CIRCLE('',#5713,1.00000000000025);
#376=CIRCLE('',#5714,1.50000000000025);
#377=CIRCLE('',#5717,0.500000000000022);
#378=CIRCLE('',#5718,1.00000000000002);
#379=CIRCLE('',#5721,0.499999999999995);
#380=CIRCLE('',#5722,0.999999999999996);
#381=CIRCLE('',#5725,0.500000000000014);
#382=CIRCLE('',#5726,1.00000000000001);
#383=CIRCLE('',#5729,0.500000000000012);
#384=CIRCLE('',#5730,1.00000000000001);
#385=CIRCLE('',#5733,1.00000000000098);
#386=CIRCLE('',#5734,1.50000000000098);
#387=CIRCLE('',#5737,100.);
#388=CIRCLE('',#5738,99.5);
#389=CIRCLE('',#5740,6.0595085413358);
#390=CIRCLE('',#5758,3.15761552865316);
#391=CIRCLE('',#5759,3.15761552865316);
#392=CIRCLE('',#5760,3.15761552865316);
#393=CIRCLE('',#5762,1.77957176368631);
#394=CIRCLE('',#5766,1.77957176368631);
#395=CIRCLE('',#5768,3.15761552865316);
#396=CIRCLE('',#5771,3.15761552865316);
#397=CIRCLE('',#5774,3.15761552865316);
#535=CYLINDRICAL_SURFACE('',#5502,1.97957176368631);
#536=CYLINDRICAL_SURFACE('',#5506,1.45);
#537=CYLINDRICAL_SURFACE('',#5510,1.97957176368631);
#538=CYLINDRICAL_SURFACE('',#5514,1.45);
#539=CYLINDRICAL_SURFACE('',#5518,1.97957176368631);
#540=CYLINDRICAL_SURFACE('',#5522,1.45);
#541=CYLINDRICAL_SURFACE('',#5526,1.97957176368631);
#542=CYLINDRICAL_SURFACE('',#5530,1.45);
#543=CYLINDRICAL_SURFACE('',#5534,1.45);
#544=CYLINDRICAL_SURFACE('',#5538,1.97957176368631);
#545=CYLINDRICAL_SURFACE('',#5542,1.45);
#546=CYLINDRICAL_SURFACE('',#5546,1.97957176368631);
#547=CYLINDRICAL_SURFACE('',#5550,1.97957176368631);
#548=CYLINDRICAL_SURFACE('',#5554,1.45);
#549=CYLINDRICAL_SURFACE('',#5558,1.97957176368631);
#550=CYLINDRICAL_SURFACE('',#5562,1.45);
#551=CYLINDRICAL_SURFACE('',#5565,1.77957176368631);
#552=CYLINDRICAL_SURFACE('',#5568,1.77957176368631);
#553=CYLINDRICAL_SURFACE('',#5645,1.50000000000039);
#554=CYLINDRICAL_SURFACE('',#5648,1.50000000000025);
#555=CYLINDRICAL_SURFACE('',#5651,1.00000000000002);
#556=CYLINDRICAL_SURFACE('',#5654,0.999999999999996);
#557=CYLINDRICAL_SURFACE('',#5657,1.00000000000001);
#558=CYLINDRICAL_SURFACE('',#5660,1.00000000000001);
#559=CYLINDRICAL_SURFACE('',#5663,1.50000000000098);
#560=CYLINDRICAL_SURFACE('',#5666,100.);
#561=CYLINDRICAL_SURFACE('',#5668,5.5595085413358);
#562=CYLINDRICAL_SURFACE('',#5670,5.5595085413358);
#563=CYLINDRICAL_SURFACE('',#5742,1.50000000000039);
#564=CYLINDRICAL_SURFACE('',#5744,1.50000000000025);
#565=CYLINDRICAL_SURFACE('',#5746,1.00000000000002);
#566=CYLINDRICAL_SURFACE('',#5748,0.999999999999996);
#567=CYLINDRICAL_SURFACE('',#5750,1.00000000000001);
#568=CYLINDRICAL_SURFACE('',#5752,1.00000000000001);
#569=CYLINDRICAL_SURFACE('',#5754,1.50000000000098);
#570=CYLINDRICAL_SURFACE('',#5756,100.);
#571=CYLINDRICAL_SURFACE('',#5769,3.15761552865316);
#572=CYLINDRICAL_SURFACE('',#5772,3.15761552865316);
#573=CYLINDRICAL_SURFACE('',#5775,3.15761552865316);
#574=CYLINDRICAL_SURFACE('',#5776,1.77957176368631);
#575=CYLINDRICAL_SURFACE('',#5777,1.77957176368631);
#576=CYLINDRICAL_SURFACE('',#5778,4.30072977423739);
#604=FACE_OUTER_BOUND('',#930,.T.);
#605=FACE_OUTER_BOUND('',#931,.T.);
#606=FACE_OUTER_BOUND('',#932,.T.);
#607=FACE_OUTER_BOUND('',#933,.T.);
#608=FACE_OUTER_BOUND('',#934,.T.);
#609=FACE_OUTER_BOUND('',#935,.T.);
#610=FACE_OUTER_BOUND('',#936,.T.);
#611=FACE_OUTER_BOUND('',#937,.T.);
#612=FACE_OUTER_BOUND('',#938,.T.);
#613=FACE_OUTER_BOUND('',#939,.T.);
#614=FACE_OUTER_BOUND('',#940,.T.);
#615=FACE_OUTER_BOUND('',#941,.T.);
#616=FACE_OUTER_BOUND('',#942,.T.);
#617=FACE_OUTER_BOUND('',#943,.T.);
#618=FACE_OUTER_BOUND('',#944,.T.);
#619=FACE_OUTER_BOUND('',#945,.T.);
#620=FACE_OUTER_BOUND('',#946,.T.);
#621=FACE_OUTER_BOUND('',#947,.T.);
#622=FACE_OUTER_BOUND('',#948,.T.);
#623=FACE_OUTER_BOUND('',#949,.T.);
#624=FACE_OUTER_BOUND('',#950,.T.);
#625=FACE_OUTER_BOUND('',#951,.T.);
#626=FACE_OUTER_BOUND('',#952,.T.);
#627=FACE_OUTER_BOUND('',#953,.T.);
#628=FACE_OUTER_BOUND('',#954,.T.);
#629=FACE_OUTER_BOUND('',#955,.T.);
#630=FACE_OUTER_BOUND('',#956,.T.);
#631=FACE_OUTER_BOUND('',#957,.T.);
#632=FACE_OUTER_BOUND('',#958,.T.);
#633=FACE_OUTER_BOUND('',#959,.T.);
#634=FACE_OUTER_BOUND('',#960,.T.);
#635=FACE_OUTER_BOUND('',#961,.T.);
#636=FACE_OUTER_BOUND('',#962,.T.);
#637=FACE_OUTER_BOUND('',#963,.T.);
#638=FACE_OUTER_BOUND('',#964,.T.);
#639=FACE_OUTER_BOUND('',#965,.T.);
#640=FACE_OUTER_BOUND('',#966,.T.);
#641=FACE_OUTER_BOUND('',#967,.T.);
#642=FACE_OUTER_BOUND('',#968,.T.);
#643=FACE_OUTER_BOUND('',#969,.T.);
#644=FACE_OUTER_BOUND('',#970,.T.);
#645=FACE_OUTER_BOUND('',#971,.T.);
#646=FACE_OUTER_BOUND('',#972,.T.);
#647=FACE_OUTER_BOUND('',#973,.T.);
#648=FACE_OUTER_BOUND('',#974,.T.);
#649=FACE_OUTER_BOUND('',#975,.T.);
#650=FACE_OUTER_BOUND('',#976,.T.);
#651=FACE_OUTER_BOUND('',#977,.T.);
#652=FACE_OUTER_BOUND('',#978,.T.);
#653=FACE_OUTER_BOUND('',#979,.T.);
#654=FACE_OUTER_BOUND('',#980,.T.);
#655=FACE_OUTER_BOUND('',#981,.T.);
#656=FACE_OUTER_BOUND('',#982,.T.);
#657=FACE_OUTER_BOUND('',#983,.T.);
#658=FACE_OUTER_BOUND('',#984,.T.);
#659=FACE_OUTER_BOUND('',#985,.T.);
#660=FACE_OUTER_BOUND('',#986,.T.);
#661=FACE_OUTER_BOUND('',#987,.T.);
#662=FACE_OUTER_BOUND('',#988,.T.);
#663=FACE_OUTER_BOUND('',#989,.T.);
#664=FACE_OUTER_BOUND('',#990,.T.);
#665=FACE_OUTER_BOUND('',#991,.T.);
#666=FACE_OUTER_BOUND('',#992,.T.);
#667=FACE_OUTER_BOUND('',#993,.T.);
#668=FACE_OUTER_BOUND('',#994,.T.);
#669=FACE_OUTER_BOUND('',#995,.T.);
#670=FACE_OUTER_BOUND('',#996,.T.);
#671=FACE_OUTER_BOUND('',#997,.T.);
#672=FACE_OUTER_BOUND('',#998,.T.);
#673=FACE_OUTER_BOUND('',#999,.T.);
#674=FACE_OUTER_BOUND('',#1000,.T.);
#675=FACE_OUTER_BOUND('',#1001,.T.);
#676=FACE_OUTER_BOUND('',#1002,.T.);
#677=FACE_OUTER_BOUND('',#1003,.T.);
#678=FACE_OUTER_BOUND('',#1004,.T.);
#679=FACE_OUTER_BOUND('',#1005,.T.);
#680=FACE_OUTER_BOUND('',#1006,.T.);
#681=FACE_OUTER_BOUND('',#1007,.T.);
#682=FACE_OUTER_BOUND('',#1008,.T.);
#683=FACE_OUTER_BOUND('',#1009,.T.);
#684=FACE_OUTER_BOUND('',#1010,.T.);
#685=FACE_OUTER_BOUND('',#1011,.T.);
#686=FACE_OUTER_BOUND('',#1012,.T.);
#687=FACE_OUTER_BOUND('',#1013,.T.);
#688=FACE_OUTER_BOUND('',#1014,.T.);
#689=FACE_OUTER_BOUND('',#1015,.T.);
#690=FACE_OUTER_BOUND('',#1016,.T.);
#691=FACE_OUTER_BOUND('',#1017,.T.);
#692=FACE_OUTER_BOUND('',#1025,.T.);
#693=FACE_OUTER_BOUND('',#1026,.T.);
#694=FACE_OUTER_BOUND('',#1027,.T.);
#695=FACE_OUTER_BOUND('',#1028,.T.);
#696=FACE_OUTER_BOUND('',#1029,.T.);
#697=FACE_OUTER_BOUND('',#1030,.T.);
#698=FACE_OUTER_BOUND('',#1031,.T.);
#699=FACE_OUTER_BOUND('',#1032,.T.);
#700=FACE_OUTER_BOUND('',#1033,.T.);
#701=FACE_OUTER_BOUND('',#1034,.T.);
#702=FACE_OUTER_BOUND('',#1035,.T.);
#703=FACE_OUTER_BOUND('',#1036,.T.);
#704=FACE_OUTER_BOUND('',#1037,.T.);
#705=FACE_OUTER_BOUND('',#1038,.T.);
#706=FACE_OUTER_BOUND('',#1039,.T.);
#707=FACE_OUTER_BOUND('',#1040,.T.);
#708=FACE_OUTER_BOUND('',#1041,.T.);
#709=FACE_OUTER_BOUND('',#1042,.T.);
#710=FACE_OUTER_BOUND('',#1043,.T.);
#711=FACE_OUTER_BOUND('',#1044,.T.);
#712=FACE_OUTER_BOUND('',#1045,.T.);
#713=FACE_OUTER_BOUND('',#1046,.T.);
#714=FACE_OUTER_BOUND('',#1047,.T.);
#715=FACE_OUTER_BOUND('',#1048,.T.);
#716=FACE_OUTER_BOUND('',#1049,.T.);
#717=FACE_OUTER_BOUND('',#1050,.T.);
#718=FACE_OUTER_BOUND('',#1051,.T.);
#719=FACE_OUTER_BOUND('',#1052,.T.);
#720=FACE_OUTER_BOUND('',#1053,.T.);
#721=FACE_OUTER_BOUND('',#1054,.T.);
#722=FACE_OUTER_BOUND('',#1055,.T.);
#723=FACE_OUTER_BOUND('',#1056,.T.);
#724=FACE_OUTER_BOUND('',#1057,.T.);
#725=FACE_OUTER_BOUND('',#1058,.T.);
#726=FACE_OUTER_BOUND('',#1059,.T.);
#727=FACE_OUTER_BOUND('',#1060,.T.);
#728=FACE_OUTER_BOUND('',#1061,.T.);
#729=FACE_OUTER_BOUND('',#1062,.T.);
#730=FACE_OUTER_BOUND('',#1063,.T.);
#731=FACE_OUTER_BOUND('',#1064,.T.);
#732=FACE_OUTER_BOUND('',#1065,.T.);
#733=FACE_OUTER_BOUND('',#1066,.T.);
#734=FACE_OUTER_BOUND('',#1067,.T.);
#735=FACE_OUTER_BOUND('',#1068,.T.);
#736=FACE_OUTER_BOUND('',#1069,.T.);
#737=FACE_OUTER_BOUND('',#1070,.T.);
#738=FACE_OUTER_BOUND('',#1071,.T.);
#739=FACE_OUTER_BOUND('',#1072,.T.);
#740=FACE_OUTER_BOUND('',#1073,.T.);
#741=FACE_OUTER_BOUND('',#1074,.T.);
#742=FACE_OUTER_BOUND('',#1075,.T.);
#743=FACE_OUTER_BOUND('',#1076,.T.);
#744=FACE_OUTER_BOUND('',#1084,.T.);
#745=FACE_OUTER_BOUND('',#1086,.T.);
#746=FACE_OUTER_BOUND('',#1088,.T.);
#747=FACE_OUTER_BOUND('',#1090,.T.);
#748=FACE_OUTER_BOUND('',#1092,.T.);
#749=FACE_OUTER_BOUND('',#1093,.T.);
#750=FACE_OUTER_BOUND('',#1094,.T.);
#751=FACE_OUTER_BOUND('',#1095,.T.);
#752=FACE_OUTER_BOUND('',#1096,.T.);
#753=FACE_OUTER_BOUND('',#1097,.T.);
#754=FACE_OUTER_BOUND('',#1098,.T.);
#755=FACE_OUTER_BOUND('',#1099,.T.);
#756=FACE_OUTER_BOUND('',#1100,.T.);
#930=EDGE_LOOP('',(#3398,#3399,#3400,#3401));
#931=EDGE_LOOP('',(#3402,#3403,#3404,#3405));
#932=EDGE_LOOP('',(#3406,#3407,#3408,#3409));
#933=EDGE_LOOP('',(#3410,#3411,#3412,#3413));
#934=EDGE_LOOP('',(#3414,#3415,#3416,#3417));
#935=EDGE_LOOP('',(#3418,#3419,#3420,#3421));
#936=EDGE_LOOP('',(#3422,#3423,#3424,#3425));
#937=EDGE_LOOP('',(#3426,#3427,#3428,#3429));
#938=EDGE_LOOP('',(#3430,#3431,#3432,#3433));
#939=EDGE_LOOP('',(#3434,#3435,#3436,#3437));
#940=EDGE_LOOP('',(#3438,#3439,#3440,#3441));
#941=EDGE_LOOP('',(#3442,#3443,#3444,#3445));
#942=EDGE_LOOP('',(#3446,#3447,#3448,#3449));
#943=EDGE_LOOP('',(#3450,#3451,#3452,#3453));
#944=EDGE_LOOP('',(#3454,#3455,#3456,#3457));
#945=EDGE_LOOP('',(#3458,#3459,#3460,#3461));
#946=EDGE_LOOP('',(#3462,#3463,#3464,#3465));
#947=EDGE_LOOP('',(#3466,#3467,#3468,#3469));
#948=EDGE_LOOP('',(#3470,#3471,#3472,#3473));
#949=EDGE_LOOP('',(#3474,#3475,#3476,#3477));
#950=EDGE_LOOP('',(#3478,#3479,#3480,#3481));
#951=EDGE_LOOP('',(#3482,#3483,#3484,#3485));
#952=EDGE_LOOP('',(#3486,#3487,#3488,#3489));
#953=EDGE_LOOP('',(#3490,#3491,#3492,#3493));
#954=EDGE_LOOP('',(#3494,#3495,#3496,#3497));
#955=EDGE_LOOP('',(#3498,#3499,#3500,#3501));
#956=EDGE_LOOP('',(#3502,#3503,#3504,#3505));
#957=EDGE_LOOP('',(#3506,#3507,#3508,#3509));
#958=EDGE_LOOP('',(#3510,#3511,#3512,#3513));
#959=EDGE_LOOP('',(#3514,#3515,#3516,#3517));
#960=EDGE_LOOP('',(#3518,#3519,#3520,#3521));
#961=EDGE_LOOP('',(#3522,#3523,#3524,#3525));
#962=EDGE_LOOP('',(#3526,#3527,#3528,#3529));
#963=EDGE_LOOP('',(#3530,#3531,#3532,#3533));
#964=EDGE_LOOP('',(#3534,#3535,#3536,#3537));
#965=EDGE_LOOP('',(#3538,#3539,#3540,#3541));
#966=EDGE_LOOP('',(#3542,#3543,#3544,#3545));
#967=EDGE_LOOP('',(#3546,#3547,#3548,#3549));
#968=EDGE_LOOP('',(#3550,#3551,#3552,#3553));
#969=EDGE_LOOP('',(#3554,#3555,#3556,#3557));
#970=EDGE_LOOP('',(#3558,#3559,#3560,#3561));
#971=EDGE_LOOP('',(#3562,#3563,#3564,#3565));
#972=EDGE_LOOP('',(#3566,#3567,#3568,#3569));
#973=EDGE_LOOP('',(#3570,#3571,#3572,#3573));
#974=EDGE_LOOP('',(#3574,#3575,#3576,#3577));
#975=EDGE_LOOP('',(#3578,#3579,#3580,#3581));
#976=EDGE_LOOP('',(#3582,#3583,#3584,#3585));
#977=EDGE_LOOP('',(#3586,#3587,#3588,#3589));
#978=EDGE_LOOP('',(#3590,#3591,#3592,#3593));
#979=EDGE_LOOP('',(#3594,#3595,#3596,#3597));
#980=EDGE_LOOP('',(#3598,#3599,#3600,#3601));
#981=EDGE_LOOP('',(#3602,#3603,#3604,#3605));
#982=EDGE_LOOP('',(#3606,#3607,#3608,#3609));
#983=EDGE_LOOP('',(#3610,#3611,#3612,#3613));
#984=EDGE_LOOP('',(#3614,#3615,#3616,#3617));
#985=EDGE_LOOP('',(#3618,#3619,#3620,#3621));
#986=EDGE_LOOP('',(#3622,#3623,#3624,#3625));
#987=EDGE_LOOP('',(#3626,#3627,#3628,#3629));
#988=EDGE_LOOP('',(#3630,#3631,#3632,#3633));
#989=EDGE_LOOP('',(#3634,#3635,#3636,#3637));
#990=EDGE_LOOP('',(#3638,#3639,#3640,#3641));
#991=EDGE_LOOP('',(#3642,#3643,#3644,#3645));
#992=EDGE_LOOP('',(#3646,#3647,#3648,#3649));
#993=EDGE_LOOP('',(#3650,#3651,#3652,#3653));
#994=EDGE_LOOP('',(#3654,#3655,#3656,#3657));
#995=EDGE_LOOP('',(#3658,#3659,#3660,#3661));
#996=EDGE_LOOP('',(#3662,#3663,#3664,#3665));
#997=EDGE_LOOP('',(#3666,#3667,#3668,#3669));
#998=EDGE_LOOP('',(#3670,#3671,#3672,#3673));
#999=EDGE_LOOP('',(#3674,#3675,#3676,#3677));
#1000=EDGE_LOOP('',(#3678,#3679,#3680,#3681));
#1001=EDGE_LOOP('',(#3682,#3683,#3684,#3685));
#1002=EDGE_LOOP('',(#3686,#3687,#3688,#3689));
#1003=EDGE_LOOP('',(#3690,#3691,#3692,#3693));
#1004=EDGE_LOOP('',(#3694,#3695,#3696,#3697));
#1005=EDGE_LOOP('',(#3698,#3699,#3700,#3701));
#1006=EDGE_LOOP('',(#3702,#3703,#3704,#3705));
#1007=EDGE_LOOP('',(#3706,#3707,#3708,#3709));
#1008=EDGE_LOOP('',(#3710,#3711,#3712,#3713));
#1009=EDGE_LOOP('',(#3714,#3715,#3716,#3717));
#1010=EDGE_LOOP('',(#3718,#3719,#3720,#3721));
#1011=EDGE_LOOP('',(#3722,#3723,#3724,#3725));
#1012=EDGE_LOOP('',(#3726,#3727,#3728,#3729));
#1013=EDGE_LOOP('',(#3730,#3731,#3732,#3733));
#1014=EDGE_LOOP('',(#3734,#3735,#3736,#3737));
#1015=EDGE_LOOP('',(#3738,#3739,#3740,#3741));
#1016=EDGE_LOOP('',(#3742,#3743,#3744,#3745));
#1017=EDGE_LOOP('',(#3746,#3747,#3748,#3749,#3750,#3751,#3752,#3753,#3754,
#3755,#3756,#3757,#3758,#3759,#3760,#3761,#3762,#3763,#3764,#3765,#3766,
#3767,#3768,#3769,#3770,#3771,#3772,#3773,#3774,#3775,#3776,#3777,#3778,
#3779,#3780));
#1018=EDGE_LOOP('',(#3781));
#1019=EDGE_LOOP('',(#3782));
#1020=EDGE_LOOP('',(#3783));
#1021=EDGE_LOOP('',(#3784));
#1022=EDGE_LOOP('',(#3785));
#1023=EDGE_LOOP('',(#3786));
#1024=EDGE_LOOP('',(#3787));
#1025=EDGE_LOOP('',(#3788,#3789,#3790,#3791));
#1026=EDGE_LOOP('',(#3792,#3793,#3794,#3795));
#1027=EDGE_LOOP('',(#3796,#3797,#3798,#3799));
#1028=EDGE_LOOP('',(#3800,#3801,#3802,#3803));
#1029=EDGE_LOOP('',(#3804,#3805,#3806,#3807));
#1030=EDGE_LOOP('',(#3808,#3809,#3810,#3811));
#1031=EDGE_LOOP('',(#3812,#3813,#3814,#3815));
#1032=EDGE_LOOP('',(#3816,#3817,#3818,#3819));
#1033=EDGE_LOOP('',(#3820,#3821,#3822,#3823));
#1034=EDGE_LOOP('',(#3824,#3825,#3826,#3827));
#1035=EDGE_LOOP('',(#3828,#3829,#3830,#3831));
#1036=EDGE_LOOP('',(#3832,#3833,#3834,#3835));
#1037=EDGE_LOOP('',(#3836,#3837,#3838,#3839));
#1038=EDGE_LOOP('',(#3840,#3841,#3842,#3843));
#1039=EDGE_LOOP('',(#3844,#3845,#3846,#3847));
#1040=EDGE_LOOP('',(#3848,#3849,#3850,#3851));
#1041=EDGE_LOOP('',(#3852,#3853,#3854,#3855));
#1042=EDGE_LOOP('',(#3856,#3857,#3858,#3859));
#1043=EDGE_LOOP('',(#3860,#3861,#3862,#3863));
#1044=EDGE_LOOP('',(#3864,#3865,#3866,#3867));
#1045=EDGE_LOOP('',(#3868,#3869,#3870,#3871));
#1046=EDGE_LOOP('',(#3872,#3873,#3874,#3875));
#1047=EDGE_LOOP('',(#3876,#3877,#3878,#3879));
#1048=EDGE_LOOP('',(#3880,#3881,#3882,#3883));
#1049=EDGE_LOOP('',(#3884,#3885,#3886,#3887));
#1050=EDGE_LOOP('',(#3888,#3889,#3890,#3891));
#1051=EDGE_LOOP('',(#3892,#3893,#3894,#3895));
#1052=EDGE_LOOP('',(#3896,#3897,#3898,#3899));
#1053=EDGE_LOOP('',(#3900,#3901,#3902,#3903));
#1054=EDGE_LOOP('',(#3904,#3905,#3906,#3907));
#1055=EDGE_LOOP('',(#3908,#3909,#3910,#3911));
#1056=EDGE_LOOP('',(#3912,#3913,#3914,#3915));
#1057=EDGE_LOOP('',(#3916,#3917,#3918,#3919));
#1058=EDGE_LOOP('',(#3920,#3921,#3922,#3923));
#1059=EDGE_LOOP('',(#3924,#3925,#3926,#3927));
#1060=EDGE_LOOP('',(#3928,#3929,#3930,#3931));
#1061=EDGE_LOOP('',(#3932,#3933,#3934,#3935));
#1062=EDGE_LOOP('',(#3936,#3937,#3938,#3939));
#1063=EDGE_LOOP('',(#3940,#3941,#3942,#3943));
#1064=EDGE_LOOP('',(#3944,#3945,#3946,#3947));
#1065=EDGE_LOOP('',(#3948,#3949,#3950,#3951));
#1066=EDGE_LOOP('',(#3952,#3953,#3954,#3955));
#1067=EDGE_LOOP('',(#3956,#3957,#3958,#3959));
#1068=EDGE_LOOP('',(#3960,#3961,#3962,#3963));
#1069=EDGE_LOOP('',(#3964,#3965,#3966,#3967));
#1070=EDGE_LOOP('',(#3968,#3969,#3970,#3971));
#1071=EDGE_LOOP('',(#3972,#3973,#3974,#3975));
#1072=EDGE_LOOP('',(#3976,#3977,#3978,#3979));
#1073=EDGE_LOOP('',(#3980,#3981,#3982,#3983));
#1074=EDGE_LOOP('',(#3984,#3985,#3986,#3987));
#1075=EDGE_LOOP('',(#3988,#3989,#3990,#3991));
#1076=EDGE_LOOP('',(#3992,#3993,#3994,#3995,#3996,#3997,#3998,#3999,#4000,
#4001,#4002,#4003,#4004,#4005,#4006,#4007,#4008,#4009,#4010,#4011,#4012,
#4013,#4014,#4015,#4016,#4017,#4018,#4019,#4020,#4021,#4022,#4023,#4024,
#4025,#4026));
#1077=EDGE_LOOP('',(#4027));
#1078=EDGE_LOOP('',(#4028));
#1079=EDGE_LOOP('',(#4029));
#1080=EDGE_LOOP('',(#4030,#4031,#4032,#4033,#4034,#4035,#4036,#4037));
#1081=EDGE_LOOP('',(#4038,#4039,#4040,#4041,#4042,#4043,#4044,#4045));
#1082=EDGE_LOOP('',(#4046,#4047,#4048,#4049,#4050,#4051,#4052,#4053));
#1083=EDGE_LOOP('',(#4054,#4055,#4056,#4057,#4058,#4059,#4060,#4061));
#1084=EDGE_LOOP('',(#4062,#4063,#4064,#4065,#4066,#4067,#4068,#4069));
#1085=EDGE_LOOP('',(#4070));
#1086=EDGE_LOOP('',(#4071,#4072,#4073,#4074,#4075,#4076,#4077,#4078));
#1087=EDGE_LOOP('',(#4079));
#1088=EDGE_LOOP('',(#4080,#4081,#4082,#4083,#4084,#4085,#4086,#4087));
#1089=EDGE_LOOP('',(#4088));
#1090=EDGE_LOOP('',(#4089,#4090,#4091,#4092,#4093,#4094,#4095,#4096));
#1091=EDGE_LOOP('',(#4097));
#1092=EDGE_LOOP('',(#4098,#4099,#4100,#4101));
#1093=EDGE_LOOP('',(#4102,#4103,#4104,#4105));
#1094=EDGE_LOOP('',(#4106,#4107,#4108,#4109));
#1095=EDGE_LOOP('',(#4110,#4111,#4112,#4113));
#1096=EDGE_LOOP('',(#4114,#4115,#4116,#4117));
#1097=EDGE_LOOP('',(#4118,#4119,#4120,#4121));
#1098=EDGE_LOOP('',(#4122,#4123,#4124,#4125));
#1099=EDGE_LOOP('',(#4126,#4127,#4128,#4129));
#1100=EDGE_LOOP('',(#4130,#4131,#4132,#4133));
#1297=LINE('',#7799,#1759);
#1298=LINE('',#7801,#1760);
#1299=LINE('',#7803,#1761);
#1300=LINE('',#7804,#1762);
#1301=LINE('',#7809,#1763);
#1302=LINE('',#7813,#1764);
#1303=LINE('',#7815,#1765);
#1304=LINE('',#7816,#1766);
#1305=LINE('',#7821,#1767);
#1306=LINE('',#7825,#1768);
#1307=LINE('',#7827,#1769);
#1308=LINE('',#7828,#1770);
#1309=LINE('',#7833,#1771);
#1310=LINE('',#7837,#1772);
#1311=LINE('',#7839,#1773);
#1312=LINE('',#7840,#1774);
#1313=LINE('',#7847,#1775);
#1314=LINE('',#7849,#1776);
#1315=LINE('',#7851,#1777);
#1316=LINE('',#7852,#1778);
#1317=LINE('',#7857,#1779);
#1318=LINE('',#7861,#1780);
#1319=LINE('',#7863,#1781);
#1320=LINE('',#7864,#1782);
#1321=LINE('',#7869,#1783);
#1322=LINE('',#7873,#1784);
#1323=LINE('',#7875,#1785);
#1324=LINE('',#7876,#1786);
#1325=LINE('',#7881,#1787);
#1326=LINE('',#7885,#1788);
#1327=LINE('',#7887,#1789);
#1328=LINE('',#7888,#1790);
#1329=LINE('',#7895,#1791);
#1330=LINE('',#7897,#1792);
#1331=LINE('',#7899,#1793);
#1332=LINE('',#7900,#1794);
#1333=LINE('',#7905,#1795);
#1334=LINE('',#7909,#1796);
#1335=LINE('',#7911,#1797);
#1336=LINE('',#7912,#1798);
#1337=LINE('',#7917,#1799);
#1338=LINE('',#7921,#1800);
#1339=LINE('',#7923,#1801);
#1340=LINE('',#7924,#1802);
#1341=LINE('',#7929,#1803);
#1342=LINE('',#7933,#1804);
#1343=LINE('',#7935,#1805);
#1344=LINE('',#7936,#1806);
#1345=LINE('',#7943,#1807);
#1346=LINE('',#7945,#1808);
#1347=LINE('',#7947,#1809);
#1348=LINE('',#7948,#1810);
#1349=LINE('',#7953,#1811);
#1350=LINE('',#7957,#1812);
#1351=LINE('',#7959,#1813);
#1352=LINE('',#7960,#1814);
#1353=LINE('',#7965,#1815);
#1354=LINE('',#7969,#1816);
#1355=LINE('',#7971,#1817);
#1356=LINE('',#7972,#1818);
#1357=LINE('',#7977,#1819);
#1358=LINE('',#7981,#1820);
#1359=LINE('',#7983,#1821);
#1360=LINE('',#7984,#1822);
#1361=LINE('',#7992,#1823);
#1362=LINE('',#7998,#1824);
#1363=LINE('',#8016,#1825);
#1364=LINE('',#8021,#1826);
#1365=LINE('',#8027,#1827);
#1366=LINE('',#8028,#1828);
#1367=LINE('',#8029,#1829);
#1368=LINE('',#8033,#1830);
#1369=LINE('',#8039,#1831);
#1370=LINE('',#8040,#1832);
#1371=LINE('',#8041,#1833);
#1372=LINE('',#8045,#1834);
#1373=LINE('',#8051,#1835);
#1374=LINE('',#8052,#1836);
#1375=LINE('',#8053,#1837);
#1376=LINE('',#8057,#1838);
#1377=LINE('',#8063,#1839);
#1378=LINE('',#8064,#1840);
#1379=LINE('',#8065,#1841);
#1380=LINE('',#8069,#1842);
#1381=LINE('',#8075,#1843);
#1382=LINE('',#8076,#1844);
#1383=LINE('',#8077,#1845);
#1384=LINE('',#8081,#1846);
#1385=LINE('',#8087,#1847);
#1386=LINE('',#8088,#1848);
#1387=LINE('',#8089,#1849);
#1388=LINE('',#8093,#1850);
#1389=LINE('',#8099,#1851);
#1390=LINE('',#8100,#1852);
#1391=LINE('',#8101,#1853);
#1392=LINE('',#8105,#1854);
#1393=LINE('',#8111,#1855);
#1394=LINE('',#8112,#1856);
#1395=LINE('',#8113,#1857);
#1396=LINE('',#8118,#1858);
#1397=LINE('',#8122,#1859);
#1398=LINE('',#8124,#1860);
#1399=LINE('',#8125,#1861);
#1400=LINE('',#8130,#1862);
#1401=LINE('',#8134,#1863);
#1402=LINE('',#8136,#1864);
#1403=LINE('',#8137,#1865);
#1404=LINE('',#8142,#1866);
#1405=LINE('',#8146,#1867);
#1406=LINE('',#8148,#1868);
#1407=LINE('',#8149,#1869);
#1408=LINE('',#8154,#1870);
#1409=LINE('',#8158,#1871);
#1410=LINE('',#8160,#1872);
#1411=LINE('',#8161,#1873);
#1412=LINE('',#8166,#1874);
#1413=LINE('',#8170,#1875);
#1414=LINE('',#8172,#1876);
#1415=LINE('',#8173,#1877);
#1416=LINE('',#8178,#1878);
#1417=LINE('',#8182,#1879);
#1418=LINE('',#8184,#1880);
#1419=LINE('',#8185,#1881);
#1420=LINE('',#8190,#1882);
#1421=LINE('',#8194,#1883);
#1422=LINE('',#8196,#1884);
#1423=LINE('',#8197,#1885);
#1424=LINE('',#8202,#1886);
#1425=LINE('',#8206,#1887);
#1426=LINE('',#8208,#1888);
#1427=LINE('',#8209,#1889);
#1428=LINE('',#8213,#1890);
#1429=LINE('',#8221,#1891);
#1430=LINE('',#8223,#1892);
#1431=LINE('',#8224,#1893);
#1432=LINE('',#8227,#1894);
#1433=LINE('',#8231,#1895);
#1434=LINE('',#8232,#1896);
#1435=LINE('',#8235,#1897);
#1436=LINE('',#8239,#1898);
#1437=LINE('',#8240,#1899);
#1438=LINE('',#8243,#1900);
#1439=LINE('',#8247,#1901);
#1440=LINE('',#8248,#1902);
#1441=LINE('',#8251,#1903);
#1442=LINE('',#8255,#1904);
#1443=LINE('',#8256,#1905);
#1444=LINE('',#8259,#1906);
#1445=LINE('',#8263,#1907);
#1446=LINE('',#8264,#1908);
#1447=LINE('',#8267,#1909);
#1448=LINE('',#8271,#1910);
#1449=LINE('',#8272,#1911);
#1450=LINE('',#8275,#1912);
#1451=LINE('',#8279,#1913);
#1452=LINE('',#8280,#1914);
#1453=LINE('',#8283,#1915);
#1454=LINE('',#8287,#1916);
#1455=LINE('',#8291,#1917);
#1456=LINE('',#8318,#1918);
#1457=LINE('',#8321,#1919);
#1458=LINE('',#8325,#1920);
#1459=LINE('',#8326,#1921);
#1460=LINE('',#8329,#1922);
#1461=LINE('',#8333,#1923);
#1462=LINE('',#8334,#1924);
#1463=LINE('',#8337,#1925);
#1464=LINE('',#8341,#1926);
#1465=LINE('',#8342,#1927);
#1466=LINE('',#8345,#1928);
#1467=LINE('',#8349,#1929);
#1468=LINE('',#8350,#1930);
#1469=LINE('',#8353,#1931);
#1470=LINE('',#8357,#1932);
#1471=LINE('',#8358,#1933);
#1472=LINE('',#8361,#1934);
#1473=LINE('',#8365,#1935);
#1474=LINE('',#8366,#1936);
#1475=LINE('',#8369,#1937);
#1476=LINE('',#8373,#1938);
#1477=LINE('',#8374,#1939);
#1478=LINE('',#8377,#1940);
#1479=LINE('',#8381,#1941);
#1480=LINE('',#8382,#1942);
#1481=LINE('',#8386,#1943);
#1482=LINE('',#8391,#1944);
#1483=LINE('',#8393,#1945);
#1484=LINE('',#8394,#1946);
#1485=LINE('',#8399,#1947);
#1486=LINE('',#8403,#1948);
#1487=LINE('',#8405,#1949);
#1488=LINE('',#8406,#1950);
#1489=LINE('',#8411,#1951);
#1490=LINE('',#8416,#1952);
#1491=LINE('',#8417,#1953);
#1492=LINE('',#8418,#1954);
#1493=LINE('',#8423,#1955);
#1494=LINE('',#8428,#1956);
#1495=LINE('',#8429,#1957);
#1496=LINE('',#8430,#1958);
#1497=LINE('',#8435,#1959);
#1498=LINE('',#8440,#1960);
#1499=LINE('',#8441,#1961);
#1500=LINE('',#8442,#1962);
#1501=LINE('',#8447,#1963);
#1502=LINE('',#8452,#1964);
#1503=LINE('',#8453,#1965);
#1504=LINE('',#8454,#1966);
#1505=LINE('',#8459,#1967);
#1506=LINE('',#8464,#1968);
#1507=LINE('',#8465,#1969);
#1508=LINE('',#8466,#1970);
#1509=LINE('',#8471,#1971);
#1510=LINE('',#8475,#1972);
#1511=LINE('',#8477,#1973);
#1512=LINE('',#8478,#1974);
#1513=LINE('',#8481,#1975);
#1514=LINE('',#8487,#1976);
#1515=LINE('',#8488,#1977);
#1516=LINE('',#8490,#1978);
#1517=LINE('',#8492,#1979);
#1518=LINE('',#8494,#1980);
#1519=LINE('',#8496,#1981);
#1520=LINE('',#8498,#1982);
#1521=LINE('',#8500,#1983);
#1522=LINE('',#8502,#1984);
#1523=LINE('',#8504,#1985);
#1524=LINE('',#8506,#1986);
#1525=LINE('',#8508,#1987);
#1526=LINE('',#8510,#1988);
#1527=LINE('',#8512,#1989);
#1528=LINE('',#8514,#1990);
#1529=LINE('',#8516,#1991);
#1530=LINE('',#8536,#1992);
#1531=LINE('',#8538,#1993);
#1532=LINE('',#8542,#1994);
#1533=LINE('',#8544,#1995);
#1534=LINE('',#8547,#1996);
#1535=LINE('',#8550,#1997);
#1536=LINE('',#8552,#1998);
#1537=LINE('',#8554,#1999);
#1759=VECTOR('',#6116,10.);
#1760=VECTOR('',#6117,10.);
#1761=VECTOR('',#6118,10.);
#1762=VECTOR('',#6119,10.);
#1763=VECTOR('',#6124,10.);
#1764=VECTOR('',#6129,10.);
#1765=VECTOR('',#6130,10.);
#1766=VECTOR('',#6131,10.);
#1767=VECTOR('',#6136,10.);
#1768=VECTOR('',#6141,10.);
#1769=VECTOR('',#6142,10.);
#1770=VECTOR('',#6143,10.);
#1771=VECTOR('',#6148,10.);
#1772=VECTOR('',#6153,10.);
#1773=VECTOR('',#6154,10.);
#1774=VECTOR('',#6155,10.);
#1775=VECTOR('',#6164,10.);
#1776=VECTOR('',#6165,10.);
#1777=VECTOR('',#6166,10.);
#1778=VECTOR('',#6167,10.);
#1779=VECTOR('',#6172,10.);
#1780=VECTOR('',#6177,10.);
#1781=VECTOR('',#6178,10.);
#1782=VECTOR('',#6179,10.);
#1783=VECTOR('',#6184,10.);
#1784=VECTOR('',#6189,10.);
#1785=VECTOR('',#6190,10.);
#1786=VECTOR('',#6191,10.);
#1787=VECTOR('',#6196,10.);
#1788=VECTOR('',#6201,10.);
#1789=VECTOR('',#6202,10.);
#1790=VECTOR('',#6203,10.);
#1791=VECTOR('',#6212,10.);
#1792=VECTOR('',#6213,10.);
#1793=VECTOR('',#6214,10.);
#1794=VECTOR('',#6215,10.);
#1795=VECTOR('',#6220,10.);
#1796=VECTOR('',#6225,10.);
#1797=VECTOR('',#6226,10.);
#1798=VECTOR('',#6227,10.);
#1799=VECTOR('',#6232,10.);
#1800=VECTOR('',#6237,10.);
#1801=VECTOR('',#6238,10.);
#1802=VECTOR('',#6239,10.);
#1803=VECTOR('',#6244,10.);
#1804=VECTOR('',#6249,10.);
#1805=VECTOR('',#6250,10.);
#1806=VECTOR('',#6251,10.);
#1807=VECTOR('',#6260,10.);
#1808=VECTOR('',#6261,10.);
#1809=VECTOR('',#6262,10.);
#1810=VECTOR('',#6263,10.);
#1811=VECTOR('',#6268,10.);
#1812=VECTOR('',#6273,10.);
#1813=VECTOR('',#6274,10.);
#1814=VECTOR('',#6275,10.);
#1815=VECTOR('',#6280,10.);
#1816=VECTOR('',#6285,10.);
#1817=VECTOR('',#6286,10.);
#1818=VECTOR('',#6287,10.);
#1819=VECTOR('',#6292,10.);
#1820=VECTOR('',#6297,10.);
#1821=VECTOR('',#6298,10.);
#1822=VECTOR('',#6299,10.);
#1823=VECTOR('',#6310,1.77957176368631);
#1824=VECTOR('',#6317,1.77957176368631);
#1825=VECTOR('',#6324,10.);
#1826=VECTOR('',#6329,10.);
#1827=VECTOR('',#6336,10.);
#1828=VECTOR('',#6337,10.);
#1829=VECTOR('',#6338,10.);
#1830=VECTOR('',#6341,10.);
#1831=VECTOR('',#6348,10.);
#1832=VECTOR('',#6349,10.);
#1833=VECTOR('',#6350,10.);
#1834=VECTOR('',#6353,10.);
#1835=VECTOR('',#6360,10.);
#1836=VECTOR('',#6361,10.);
#1837=VECTOR('',#6362,10.);
#1838=VECTOR('',#6365,10.);
#1839=VECTOR('',#6372,10.);
#1840=VECTOR('',#6373,10.);
#1841=VECTOR('',#6374,10.);
#1842=VECTOR('',#6377,10.);
#1843=VECTOR('',#6384,10.);
#1844=VECTOR('',#6385,10.);
#1845=VECTOR('',#6386,10.);
#1846=VECTOR('',#6389,10.);
#1847=VECTOR('',#6396,10.);
#1848=VECTOR('',#6397,10.);
#1849=VECTOR('',#6398,10.);
#1850=VECTOR('',#6401,10.);
#1851=VECTOR('',#6408,10.);
#1852=VECTOR('',#6409,10.);
#1853=VECTOR('',#6410,10.);
#1854=VECTOR('',#6413,10.);
#1855=VECTOR('',#6420,10.);
#1856=VECTOR('',#6421,10.);
#1857=VECTOR('',#6422,10.);
#1858=VECTOR('',#6427,10.);
#1859=VECTOR('',#6432,10.);
#1860=VECTOR('',#6433,10.);
#1861=VECTOR('',#6434,10.);
#1862=VECTOR('',#6439,10.);
#1863=VECTOR('',#6444,10.);
#1864=VECTOR('',#6445,10.);
#1865=VECTOR('',#6446,10.);
#1866=VECTOR('',#6451,10.);
#1867=VECTOR('',#6456,10.);
#1868=VECTOR('',#6457,10.);
#1869=VECTOR('',#6458,10.);
#1870=VECTOR('',#6463,10.);
#1871=VECTOR('',#6468,10.);
#1872=VECTOR('',#6469,10.);
#1873=VECTOR('',#6470,10.);
#1874=VECTOR('',#6475,10.);
#1875=VECTOR('',#6480,10.);
#1876=VECTOR('',#6481,10.);
#1877=VECTOR('',#6482,10.);
#1878=VECTOR('',#6487,10.);
#1879=VECTOR('',#6492,10.);
#1880=VECTOR('',#6493,10.);
#1881=VECTOR('',#6494,10.);
#1882=VECTOR('',#6499,10.);
#1883=VECTOR('',#6504,10.);
#1884=VECTOR('',#6505,10.);
#1885=VECTOR('',#6506,10.);
#1886=VECTOR('',#6511,10.);
#1887=VECTOR('',#6516,10.);
#1888=VECTOR('',#6517,10.);
#1889=VECTOR('',#6518,10.);
#1890=VECTOR('',#6521,10.);
#1891=VECTOR('',#6534,10.);
#1892=VECTOR('',#6535,10.);
#1893=VECTOR('',#6536,10.);
#1894=VECTOR('',#6539,10.);
#1895=VECTOR('',#6544,10.);
#1896=VECTOR('',#6545,10.);
#1897=VECTOR('',#6548,10.);
#1898=VECTOR('',#6553,10.);
#1899=VECTOR('',#6554,10.);
#1900=VECTOR('',#6557,10.);
#1901=VECTOR('',#6562,10.);
#1902=VECTOR('',#6563,10.);
#1903=VECTOR('',#6566,10.);
#1904=VECTOR('',#6571,10.);
#1905=VECTOR('',#6572,10.);
#1906=VECTOR('',#6575,10.);
#1907=VECTOR('',#6580,10.);
#1908=VECTOR('',#6581,10.);
#1909=VECTOR('',#6584,10.);
#1910=VECTOR('',#6589,10.);
#1911=VECTOR('',#6590,10.);
#1912=VECTOR('',#6593,10.);
#1913=VECTOR('',#6598,10.);
#1914=VECTOR('',#6599,10.);
#1915=VECTOR('',#6602,10.);
#1916=VECTOR('',#6607,10.);
#1917=VECTOR('',#6612,10.);
#1918=VECTOR('',#6631,10.);
#1919=VECTOR('',#6634,10.);
#1920=VECTOR('',#6639,10.);
#1921=VECTOR('',#6640,10.);
#1922=VECTOR('',#6643,10.);
#1923=VECTOR('',#6648,10.);
#1924=VECTOR('',#6649,10.);
#1925=VECTOR('',#6652,10.);
#1926=VECTOR('',#6657,10.);
#1927=VECTOR('',#6658,10.);
#1928=VECTOR('',#6661,10.);
#1929=VECTOR('',#6666,10.);
#1930=VECTOR('',#6667,10.);
#1931=VECTOR('',#6670,10.);
#1932=VECTOR('',#6675,10.);
#1933=VECTOR('',#6676,10.);
#1934=VECTOR('',#6679,10.);
#1935=VECTOR('',#6684,10.);
#1936=VECTOR('',#6685,10.);
#1937=VECTOR('',#6688,10.);
#1938=VECTOR('',#6693,10.);
#1939=VECTOR('',#6694,10.);
#1940=VECTOR('',#6697,10.);
#1941=VECTOR('',#6702,10.);
#1942=VECTOR('',#6703,10.);
#1943=VECTOR('',#6706,10.);
#1944=VECTOR('',#6713,10.);
#1945=VECTOR('',#6714,10.);
#1946=VECTOR('',#6715,10.);
#1947=VECTOR('',#6720,10.);
#1948=VECTOR('',#6725,10.);
#1949=VECTOR('',#6726,10.);
#1950=VECTOR('',#6727,10.);
#1951=VECTOR('',#6732,10.);
#1952=VECTOR('',#6737,10.);
#1953=VECTOR('',#6738,10.);
#1954=VECTOR('',#6739,10.);
#1955=VECTOR('',#6744,10.);
#1956=VECTOR('',#6749,10.);
#1957=VECTOR('',#6750,10.);
#1958=VECTOR('',#6751,10.);
#1959=VECTOR('',#6756,10.);
#1960=VECTOR('',#6761,10.);
#1961=VECTOR('',#6762,10.);
#1962=VECTOR('',#6763,10.);
#1963=VECTOR('',#6768,10.);
#1964=VECTOR('',#6773,10.);
#1965=VECTOR('',#6774,10.);
#1966=VECTOR('',#6775,10.);
#1967=VECTOR('',#6780,10.);
#1968=VECTOR('',#6785,10.);
#1969=VECTOR('',#6786,10.);
#1970=VECTOR('',#6787,10.);
#1971=VECTOR('',#6792,10.);
#1972=VECTOR('',#6797,10.);
#1973=VECTOR('',#6798,10.);
#1974=VECTOR('',#6799,10.);
#1975=VECTOR('',#6802,10.);
#1976=VECTOR('',#6813,10.);
#1977=VECTOR('',#6814,10.);
#1978=VECTOR('',#6817,10.);
#1979=VECTOR('',#6820,10.);
#1980=VECTOR('',#6823,10.);
#1981=VECTOR('',#6826,10.);
#1982=VECTOR('',#6829,10.);
#1983=VECTOR('',#6832,10.);
#1984=VECTOR('',#6835,10.);
#1985=VECTOR('',#6838,10.);
#1986=VECTOR('',#6841,10.);
#1987=VECTOR('',#6844,10.);
#1988=VECTOR('',#6847,10.);
#1989=VECTOR('',#6850,10.);
#1990=VECTOR('',#6853,10.);
#1991=VECTOR('',#6856,10.);
#1992=VECTOR('',#6883,3.40761552865316);
#1993=VECTOR('',#6886,3.15761552865316);
#1994=VECTOR('',#6891,3.40761552865316);
#1995=VECTOR('',#6894,3.15761552865316);
#1996=VECTOR('',#6897,3.40761552865316);
#1997=VECTOR('',#6902,3.15761552865316);
#1998=VECTOR('',#6905,1.77957176368631);
#1999=VECTOR('',#6908,1.77957176368631);
#2221=VERTEX_POINT('',#7797);
#2222=VERTEX_POINT('',#7798);
#2223=VERTEX_POINT('',#7800);
#2224=VERTEX_POINT('',#7802);
#2225=VERTEX_POINT('',#7806);
#2226=VERTEX_POINT('',#7808);
#2227=VERTEX_POINT('',#7812);
#2228=VERTEX_POINT('',#7814);
#2229=VERTEX_POINT('',#7818);
#2230=VERTEX_POINT('',#7820);
#2231=VERTEX_POINT('',#7824);
#2232=VERTEX_POINT('',#7826);
#2233=VERTEX_POINT('',#7830);
#2234=VERTEX_POINT('',#7832);
#2235=VERTEX_POINT('',#7836);
#2236=VERTEX_POINT('',#7838);
#2237=VERTEX_POINT('',#7845);
#2238=VERTEX_POINT('',#7846);
#2239=VERTEX_POINT('',#7848);
#2240=VERTEX_POINT('',#7850);
#2241=VERTEX_POINT('',#7854);
#2242=VERTEX_POINT('',#7856);
#2243=VERTEX_POINT('',#7860);
#2244=VERTEX_POINT('',#7862);
#2245=VERTEX_POINT('',#7866);
#2246=VERTEX_POINT('',#7868);
#2247=VERTEX_POINT('',#7872);
#2248=VERTEX_POINT('',#7874);
#2249=VERTEX_POINT('',#7878);
#2250=VERTEX_POINT('',#7880);
#2251=VERTEX_POINT('',#7884);
#2252=VERTEX_POINT('',#7886);
#2253=VERTEX_POINT('',#7893);
#2254=VERTEX_POINT('',#7894);
#2255=VERTEX_POINT('',#7896);
#2256=VERTEX_POINT('',#7898);
#2257=VERTEX_POINT('',#7902);
#2258=VERTEX_POINT('',#7904);
#2259=VERTEX_POINT('',#7908);
#2260=VERTEX_POINT('',#7910);
#2261=VERTEX_POINT('',#7914);
#2262=VERTEX_POINT('',#7916);
#2263=VERTEX_POINT('',#7920);
#2264=VERTEX_POINT('',#7922);
#2265=VERTEX_POINT('',#7926);
#2266=VERTEX_POINT('',#7928);
#2267=VERTEX_POINT('',#7932);
#2268=VERTEX_POINT('',#7934);
#2269=VERTEX_POINT('',#7941);
#2270=VERTEX_POINT('',#7942);
#2271=VERTEX_POINT('',#7944);
#2272=VERTEX_POINT('',#7946);
#2273=VERTEX_POINT('',#7950);
#2274=VERTEX_POINT('',#7952);
#2275=VERTEX_POINT('',#7956);
#2276=VERTEX_POINT('',#7958);
#2277=VERTEX_POINT('',#7962);
#2278=VERTEX_POINT('',#7964);
#2279=VERTEX_POINT('',#7968);
#2280=VERTEX_POINT('',#7970);
#2281=VERTEX_POINT('',#7974);
#2282=VERTEX_POINT('',#7976);
#2283=VERTEX_POINT('',#7980);
#2284=VERTEX_POINT('',#7982);
#2285=VERTEX_POINT('',#7989);
#2286=VERTEX_POINT('',#7991);
#2287=VERTEX_POINT('',#7995);
#2288=VERTEX_POINT('',#7997);
#2289=VERTEX_POINT('',#8001);
#2290=VERTEX_POINT('',#8002);
#2291=VERTEX_POINT('',#8013);
#2292=VERTEX_POINT('',#8015);
#2293=VERTEX_POINT('',#8019);
#2294=VERTEX_POINT('',#8020);
#2295=VERTEX_POINT('',#8025);
#2296=VERTEX_POINT('',#8026);
#2297=VERTEX_POINT('',#8031);
#2298=VERTEX_POINT('',#8032);
#2299=VERTEX_POINT('',#8037);
#2300=VERTEX_POINT('',#8038);
#2301=VERTEX_POINT('',#8043);
#2302=VERTEX_POINT('',#8044);
#2303=VERTEX_POINT('',#8049);
#2304=VERTEX_POINT('',#8050);
#2305=VERTEX_POINT('',#8055);
#2306=VERTEX_POINT('',#8056);
#2307=VERTEX_POINT('',#8061);
#2308=VERTEX_POINT('',#8062);
#2309=VERTEX_POINT('',#8067);
#2310=VERTEX_POINT('',#8068);
#2311=VERTEX_POINT('',#8073);
#2312=VERTEX_POINT('',#8074);
#2313=VERTEX_POINT('',#8079);
#2314=VERTEX_POINT('',#8080);
#2315=VERTEX_POINT('',#8085);
#2316=VERTEX_POINT('',#8086);
#2317=VERTEX_POINT('',#8091);
#2318=VERTEX_POINT('',#8092);
#2319=VERTEX_POINT('',#8097);
#2320=VERTEX_POINT('',#8098);
#2321=VERTEX_POINT('',#8103);
#2322=VERTEX_POINT('',#8104);
#2323=VERTEX_POINT('',#8109);
#2324=VERTEX_POINT('',#8110);
#2325=VERTEX_POINT('',#8115);
#2326=VERTEX_POINT('',#8117);
#2327=VERTEX_POINT('',#8121);
#2328=VERTEX_POINT('',#8123);
#2329=VERTEX_POINT('',#8127);
#2330=VERTEX_POINT('',#8129);
#2331=VERTEX_POINT('',#8133);
#2332=VERTEX_POINT('',#8135);
#2333=VERTEX_POINT('',#8139);
#2334=VERTEX_POINT('',#8141);
#2335=VERTEX_POINT('',#8145);
#2336=VERTEX_POINT('',#8147);
#2337=VERTEX_POINT('',#8151);
#2338=VERTEX_POINT('',#8153);
#2339=VERTEX_POINT('',#8157);
#2340=VERTEX_POINT('',#8159);
#2341=VERTEX_POINT('',#8163);
#2342=VERTEX_POINT('',#8165);
#2343=VERTEX_POINT('',#8169);
#2344=VERTEX_POINT('',#8171);
#2345=VERTEX_POINT('',#8175);
#2346=VERTEX_POINT('',#8177);
#2347=VERTEX_POINT('',#8181);
#2348=VERTEX_POINT('',#8183);
#2349=VERTEX_POINT('',#8187);
#2350=VERTEX_POINT('',#8189);
#2351=VERTEX_POINT('',#8193);
#2352=VERTEX_POINT('',#8195);
#2353=VERTEX_POINT('',#8199);
#2354=VERTEX_POINT('',#8201);
#2355=VERTEX_POINT('',#8205);
#2356=VERTEX_POINT('',#8207);
#2357=VERTEX_POINT('',#8211);
#2358=VERTEX_POINT('',#8212);
#2359=VERTEX_POINT('',#8220);
#2360=VERTEX_POINT('',#8222);
#2361=VERTEX_POINT('',#8226);
#2362=VERTEX_POINT('',#8230);
#2363=VERTEX_POINT('',#8234);
#2364=VERTEX_POINT('',#8238);
#2365=VERTEX_POINT('',#8242);
#2366=VERTEX_POINT('',#8246);
#2367=VERTEX_POINT('',#8250);
#2368=VERTEX_POINT('',#8254);
#2369=VERTEX_POINT('',#8258);
#2370=VERTEX_POINT('',#8262);
#2371=VERTEX_POINT('',#8266);
#2372=VERTEX_POINT('',#8270);
#2373=VERTEX_POINT('',#8274);
#2374=VERTEX_POINT('',#8278);
#2375=VERTEX_POINT('',#8282);
#2376=VERTEX_POINT('',#8286);
#2377=VERTEX_POINT('',#8290);
#2378=VERTEX_POINT('',#8294);
#2379=VERTEX_POINT('',#8296);
#2380=VERTEX_POINT('',#8298);
#2381=VERTEX_POINT('',#8300);
#2382=VERTEX_POINT('',#8302);
#2383=VERTEX_POINT('',#8305);
#2384=VERTEX_POINT('',#8316);
#2385=VERTEX_POINT('',#8320);
#2386=VERTEX_POINT('',#8324);
#2387=VERTEX_POINT('',#8328);
#2388=VERTEX_POINT('',#8332);
#2389=VERTEX_POINT('',#8336);
#2390=VERTEX_POINT('',#8340);
#2391=VERTEX_POINT('',#8344);
#2392=VERTEX_POINT('',#8348);
#2393=VERTEX_POINT('',#8352);
#2394=VERTEX_POINT('',#8356);
#2395=VERTEX_POINT('',#8360);
#2396=VERTEX_POINT('',#8364);
#2397=VERTEX_POINT('',#8368);
#2398=VERTEX_POINT('',#8372);
#2399=VERTEX_POINT('',#8376);
#2400=VERTEX_POINT('',#8380);
#2401=VERTEX_POINT('',#8384);
#2402=VERTEX_POINT('',#8385);
#2403=VERTEX_POINT('',#8390);
#2404=VERTEX_POINT('',#8392);
#2405=VERTEX_POINT('',#8396);
#2406=VERTEX_POINT('',#8398);
#2407=VERTEX_POINT('',#8402);
#2408=VERTEX_POINT('',#8404);
#2409=VERTEX_POINT('',#8408);
#2410=VERTEX_POINT('',#8410);
#2411=VERTEX_POINT('',#8414);
#2412=VERTEX_POINT('',#8415);
#2413=VERTEX_POINT('',#8420);
#2414=VERTEX_POINT('',#8422);
#2415=VERTEX_POINT('',#8426);
#2416=VERTEX_POINT('',#8427);
#2417=VERTEX_POINT('',#8432);
#2418=VERTEX_POINT('',#8434);
#2419=VERTEX_POINT('',#8438);
#2420=VERTEX_POINT('',#8439);
#2421=VERTEX_POINT('',#8444);
#2422=VERTEX_POINT('',#8446);
#2423=VERTEX_POINT('',#8450);
#2424=VERTEX_POINT('',#8451);
#2425=VERTEX_POINT('',#8456);
#2426=VERTEX_POINT('',#8458);
#2427=VERTEX_POINT('',#8462);
#2428=VERTEX_POINT('',#8463);
#2429=VERTEX_POINT('',#8468);
#2430=VERTEX_POINT('',#8470);
#2431=VERTEX_POINT('',#8474);
#2432=VERTEX_POINT('',#8476);
#2433=VERTEX_POINT('',#8480);
#2434=VERTEX_POINT('',#8519);
#2435=VERTEX_POINT('',#8521);
#2436=VERTEX_POINT('',#8523);
#2437=VERTEX_POINT('',#8526);
#2438=VERTEX_POINT('',#8531);
#2439=VERTEX_POINT('',#8534);
#2440=VERTEX_POINT('',#8540);
#2441=VERTEX_POINT('',#8546);
#2664=EDGE_CURVE('',#2221,#2222,#1297,.T.);
#2665=EDGE_CURVE('',#2221,#2223,#1298,.T.);
#2666=EDGE_CURVE('',#2223,#2224,#1299,.T.);
#2667=EDGE_CURVE('',#2222,#2224,#1300,.T.);
#2668=EDGE_CURVE('',#2225,#2221,#273,.T.);
#2669=EDGE_CURVE('',#2225,#2226,#1301,.T.);
#2670=EDGE_CURVE('',#2226,#2223,#274,.T.);
#2671=EDGE_CURVE('',#2227,#2225,#1302,.T.);
#2672=EDGE_CURVE('',#2227,#2228,#1303,.T.);
#2673=EDGE_CURVE('',#2228,#2226,#1304,.T.);
#2674=EDGE_CURVE('',#2229,#2227,#275,.T.);
#2675=EDGE_CURVE('',#2229,#2230,#1305,.T.);
#2676=EDGE_CURVE('',#2230,#2228,#276,.T.);
#2677=EDGE_CURVE('',#2231,#2229,#1306,.T.);
#2678=EDGE_CURVE('',#2231,#2232,#1307,.T.);
#2679=EDGE_CURVE('',#2232,#2230,#1308,.T.);
#2680=EDGE_CURVE('',#2233,#2231,#277,.T.);
#2681=EDGE_CURVE('',#2233,#2234,#1309,.T.);
#2682=EDGE_CURVE('',#2234,#2232,#278,.T.);
#2683=EDGE_CURVE('',#2235,#2233,#1310,.T.);
#2684=EDGE_CURVE('',#2235,#2236,#1311,.T.);
#2685=EDGE_CURVE('',#2236,#2234,#1312,.T.);
#2686=EDGE_CURVE('',#2222,#2235,#279,.T.);
#2687=EDGE_CURVE('',#2224,#2236,#280,.T.);
#2688=EDGE_CURVE('',#2237,#2238,#1313,.T.);
#2689=EDGE_CURVE('',#2237,#2239,#1314,.T.);
#2690=EDGE_CURVE('',#2239,#2240,#1315,.T.);
#2691=EDGE_CURVE('',#2238,#2240,#1316,.T.);
#2692=EDGE_CURVE('',#2241,#2237,#281,.T.);
#2693=EDGE_CURVE('',#2241,#2242,#1317,.T.);
#2694=EDGE_CURVE('',#2242,#2239,#282,.T.);
#2695=EDGE_CURVE('',#2243,#2241,#1318,.T.);
#2696=EDGE_CURVE('',#2243,#2244,#1319,.T.);
#2697=EDGE_CURVE('',#2244,#2242,#1320,.T.);
#2698=EDGE_CURVE('',#2245,#2243,#283,.T.);
#2699=EDGE_CURVE('',#2245,#2246,#1321,.T.);
#2700=EDGE_CURVE('',#2246,#2244,#284,.T.);
#2701=EDGE_CURVE('',#2247,#2245,#1322,.T.);
#2702=EDGE_CURVE('',#2247,#2248,#1323,.T.);
#2703=EDGE_CURVE('',#2248,#2246,#1324,.T.);
#2704=EDGE_CURVE('',#2249,#2247,#285,.T.);
#2705=EDGE_CURVE('',#2249,#2250,#1325,.T.);
#2706=EDGE_CURVE('',#2250,#2248,#286,.T.);
#2707=EDGE_CURVE('',#2251,#2249,#1326,.T.);
#2708=EDGE_CURVE('',#2251,#2252,#1327,.T.);
#2709=EDGE_CURVE('',#2252,#2250,#1328,.T.);
#2710=EDGE_CURVE('',#2238,#2251,#287,.T.);
#2711=EDGE_CURVE('',#2240,#2252,#288,.T.);
#2712=EDGE_CURVE('',#2253,#2254,#1329,.T.);
#2713=EDGE_CURVE('',#2253,#2255,#1330,.T.);
#2714=EDGE_CURVE('',#2255,#2256,#1331,.T.);
#2715=EDGE_CURVE('',#2254,#2256,#1332,.T.);
#2716=EDGE_CURVE('',#2257,#2253,#289,.T.);
#2717=EDGE_CURVE('',#2257,#2258,#1333,.T.);
#2718=EDGE_CURVE('',#2258,#2255,#290,.T.);
#2719=EDGE_CURVE('',#2259,#2257,#1334,.T.);
#2720=EDGE_CURVE('',#2259,#2260,#1335,.T.);
#2721=EDGE_CURVE('',#2260,#2258,#1336,.T.);
#2722=EDGE_CURVE('',#2261,#2259,#291,.T.);
#2723=EDGE_CURVE('',#2261,#2262,#1337,.T.);
#2724=EDGE_CURVE('',#2262,#2260,#292,.T.);
#2725=EDGE_CURVE('',#2263,#2261,#1338,.T.);
#2726=EDGE_CURVE('',#2263,#2264,#1339,.T.);
#2727=EDGE_CURVE('',#2264,#2262,#1340,.T.);
#2728=EDGE_CURVE('',#2265,#2263,#293,.T.);
#2729=EDGE_CURVE('',#2265,#2266,#1341,.T.);
#2730=EDGE_CURVE('',#2266,#2264,#294,.T.);
#2731=EDGE_CURVE('',#2267,#2265,#1342,.T.);
#2732=EDGE_CURVE('',#2267,#2268,#1343,.T.);
#2733=EDGE_CURVE('',#2268,#2266,#1344,.T.);
#2734=EDGE_CURVE('',#2254,#2267,#295,.T.);
#2735=EDGE_CURVE('',#2256,#2268,#296,.T.);
#2736=EDGE_CURVE('',#2269,#2270,#1345,.T.);
#2737=EDGE_CURVE('',#2269,#2271,#1346,.T.);
#2738=EDGE_CURVE('',#2271,#2272,#1347,.T.);
#2739=EDGE_CURVE('',#2270,#2272,#1348,.T.);
#2740=EDGE_CURVE('',#2273,#2269,#297,.T.);
#2741=EDGE_CURVE('',#2273,#2274,#1349,.T.);
#2742=EDGE_CURVE('',#2274,#2271,#298,.T.);
#2743=EDGE_CURVE('',#2275,#2273,#1350,.T.);
#2744=EDGE_CURVE('',#2275,#2276,#1351,.T.);
#2745=EDGE_CURVE('',#2276,#2274,#1352,.T.);
#2746=EDGE_CURVE('',#2277,#2275,#299,.T.);
#2747=EDGE_CURVE('',#2277,#2278,#1353,.T.);
#2748=EDGE_CURVE('',#2278,#2276,#300,.T.);
#2749=EDGE_CURVE('',#2279,#2277,#1354,.T.);
#2750=EDGE_CURVE('',#2279,#2280,#1355,.T.);
#2751=EDGE_CURVE('',#2280,#2278,#1356,.T.);
#2752=EDGE_CURVE('',#2281,#2279,#301,.T.);
#2753=EDGE_CURVE('',#2281,#2282,#1357,.T.);
#2754=EDGE_CURVE('',#2282,#2280,#302,.T.);
#2755=EDGE_CURVE('',#2283,#2281,#1358,.T.);
#2756=EDGE_CURVE('',#2283,#2284,#1359,.T.);
#2757=EDGE_CURVE('',#2284,#2282,#1360,.T.);
#2758=EDGE_CURVE('',#2270,#2283,#303,.T.);
#2759=EDGE_CURVE('',#2272,#2284,#304,.T.);
#2760=EDGE_CURVE('',#2285,#2285,#305,.T.);
#2761=EDGE_CURVE('',#2285,#2286,#1361,.T.);
#2762=EDGE_CURVE('',#2286,#2286,#306,.T.);
#2763=EDGE_CURVE('',#2287,#2287,#307,.T.);
#2764=EDGE_CURVE('',#2287,#2288,#1362,.T.);
#2765=EDGE_CURVE('',#2288,#2288,#308,.T.);
#2766=EDGE_CURVE('',#2289,#2290,#173,.T.);
#2767=EDGE_CURVE('',#2290,#2291,#309,.T.);
#2768=EDGE_CURVE('',#2291,#2292,#1363,.T.);
#2769=EDGE_CURVE('',#2292,#2289,#310,.T.);
#2770=EDGE_CURVE('',#2293,#2294,#1364,.T.);
#2771=EDGE_CURVE('',#2294,#2292,#311,.T.);
#2772=EDGE_CURVE('',#2291,#2293,#312,.T.);
#2773=EDGE_CURVE('',#2295,#2296,#1365,.T.);
#2774=EDGE_CURVE('',#2296,#2294,#1366,.T.);
#2775=EDGE_CURVE('',#2293,#2295,#1367,.T.);
#2776=EDGE_CURVE('',#2297,#2298,#1368,.T.);
#2777=EDGE_CURVE('',#2298,#2296,#313,.T.);
#2778=EDGE_CURVE('',#2295,#2297,#314,.T.);
#2779=EDGE_CURVE('',#2299,#2300,#1369,.T.);
#2780=EDGE_CURVE('',#2300,#2298,#1370,.T.);
#2781=EDGE_CURVE('',#2297,#2299,#1371,.T.);
#2782=EDGE_CURVE('',#2301,#2302,#1372,.T.);
#2783=EDGE_CURVE('',#2302,#2300,#315,.T.);
#2784=EDGE_CURVE('',#2299,#2301,#316,.T.);
#2785=EDGE_CURVE('',#2303,#2304,#1373,.T.);
#2786=EDGE_CURVE('',#2304,#2302,#1374,.T.);
#2787=EDGE_CURVE('',#2301,#2303,#1375,.T.);
#2788=EDGE_CURVE('',#2305,#2306,#1376,.T.);
#2789=EDGE_CURVE('',#2306,#2304,#317,.T.);
#2790=EDGE_CURVE('',#2303,#2305,#318,.T.);
#2791=EDGE_CURVE('',#2307,#2308,#1377,.T.);
#2792=EDGE_CURVE('',#2308,#2306,#1378,.T.);
#2793=EDGE_CURVE('',#2305,#2307,#1379,.T.);
#2794=EDGE_CURVE('',#2309,#2310,#1380,.T.);
#2795=EDGE_CURVE('',#2310,#2308,#319,.T.);
#2796=EDGE_CURVE('',#2307,#2309,#320,.T.);
#2797=EDGE_CURVE('',#2311,#2312,#1381,.T.);
#2798=EDGE_CURVE('',#2312,#2310,#1382,.T.);
#2799=EDGE_CURVE('',#2309,#2311,#1383,.T.);
#2800=EDGE_CURVE('',#2313,#2314,#1384,.T.);
#2801=EDGE_CURVE('',#2314,#2312,#321,.T.);
#2802=EDGE_CURVE('',#2311,#2313,#322,.T.);
#2803=EDGE_CURVE('',#2315,#2316,#1385,.T.);
#2804=EDGE_CURVE('',#2316,#2314,#1386,.T.);
#2805=EDGE_CURVE('',#2313,#2315,#1387,.T.);
#2806=EDGE_CURVE('',#2317,#2318,#1388,.T.);
#2807=EDGE_CURVE('',#2318,#2316,#323,.T.);
#2808=EDGE_CURVE('',#2315,#2317,#324,.T.);
#2809=EDGE_CURVE('',#2319,#2320,#1389,.T.);
#2810=EDGE_CURVE('',#2320,#2318,#1390,.T.);
#2811=EDGE_CURVE('',#2317,#2319,#1391,.T.);
#2812=EDGE_CURVE('',#2321,#2322,#1392,.T.);
#2813=EDGE_CURVE('',#2322,#2320,#325,.T.);
#2814=EDGE_CURVE('',#2319,#2321,#326,.T.);
#2815=EDGE_CURVE('',#2323,#2324,#1393,.T.);
#2816=EDGE_CURVE('',#2324,#2322,#1394,.T.);
#2817=EDGE_CURVE('',#2321,#2323,#1395,.T.);
#2818=EDGE_CURVE('',#2323,#2325,#327,.T.);
#2819=EDGE_CURVE('',#2325,#2326,#1396,.T.);
#2820=EDGE_CURVE('',#2326,#2324,#328,.T.);
#2821=EDGE_CURVE('',#2325,#2327,#1397,.T.);
#2822=EDGE_CURVE('',#2327,#2328,#1398,.T.);
#2823=EDGE_CURVE('',#2328,#2326,#1399,.T.);
#2824=EDGE_CURVE('',#2327,#2329,#329,.T.);
#2825=EDGE_CURVE('',#2329,#2330,#1400,.T.);
#2826=EDGE_CURVE('',#2330,#2328,#330,.T.);
#2827=EDGE_CURVE('',#2329,#2331,#1401,.T.);
#2828=EDGE_CURVE('',#2331,#2332,#1402,.T.);
#2829=EDGE_CURVE('',#2332,#2330,#1403,.T.);
#2830=EDGE_CURVE('',#2331,#2333,#331,.T.);
#2831=EDGE_CURVE('',#2333,#2334,#1404,.T.);
#2832=EDGE_CURVE('',#2334,#2332,#332,.T.);
#2833=EDGE_CURVE('',#2333,#2335,#1405,.T.);
#2834=EDGE_CURVE('',#2335,#2336,#1406,.T.);
#2835=EDGE_CURVE('',#2336,#2334,#1407,.T.);
#2836=EDGE_CURVE('',#2335,#2337,#333,.T.);
#2837=EDGE_CURVE('',#2337,#2338,#1408,.T.);
#2838=EDGE_CURVE('',#2338,#2336,#334,.T.);
#2839=EDGE_CURVE('',#2337,#2339,#1409,.T.);
#2840=EDGE_CURVE('',#2339,#2340,#1410,.T.);
#2841=EDGE_CURVE('',#2340,#2338,#1411,.T.);
#2842=EDGE_CURVE('',#2339,#2341,#335,.T.);
#2843=EDGE_CURVE('',#2341,#2342,#1412,.T.);
#2844=EDGE_CURVE('',#2342,#2340,#336,.T.);
#2845=EDGE_CURVE('',#2341,#2343,#1413,.T.);
#2846=EDGE_CURVE('',#2343,#2344,#1414,.T.);
#2847=EDGE_CURVE('',#2344,#2342,#1415,.T.);
#2848=EDGE_CURVE('',#2343,#2345,#337,.T.);
#2849=EDGE_CURVE('',#2345,#2346,#1416,.T.);
#2850=EDGE_CURVE('',#2346,#2344,#338,.T.);
#2851=EDGE_CURVE('',#2345,#2347,#1417,.T.);
#2852=EDGE_CURVE('',#2347,#2348,#1418,.T.);
#2853=EDGE_CURVE('',#2348,#2346,#1419,.T.);
#2854=EDGE_CURVE('',#2347,#2349,#339,.T.);
#2855=EDGE_CURVE('',#2349,#2350,#1420,.T.);
#2856=EDGE_CURVE('',#2350,#2348,#340,.T.);
#2857=EDGE_CURVE('',#2349,#2351,#1421,.T.);
#2858=EDGE_CURVE('',#2351,#2352,#1422,.T.);
#2859=EDGE_CURVE('',#2352,#2350,#1423,.T.);
#2860=EDGE_CURVE('',#2351,#2353,#341,.T.);
#2861=EDGE_CURVE('',#2353,#2354,#1424,.T.);
#2862=EDGE_CURVE('',#2354,#2352,#342,.T.);
#2863=EDGE_CURVE('',#2353,#2355,#1425,.T.);
#2864=EDGE_CURVE('',#2355,#2356,#1426,.T.);
#2865=EDGE_CURVE('',#2356,#2354,#1427,.T.);
#2866=EDGE_CURVE('',#2357,#2358,#1428,.T.);
#2867=EDGE_CURVE('',#2358,#2356,#343,.T.);
#2868=EDGE_CURVE('',#2355,#2357,#344,.T.);
#2869=EDGE_CURVE('',#2289,#2358,#345,.T.);
#2870=EDGE_CURVE('',#2357,#2290,#346,.T.);
#2871=EDGE_CURVE('',#2359,#2328,#1429,.T.);
#2872=EDGE_CURVE('',#2360,#2359,#1430,.T.);
#2873=EDGE_CURVE('',#2360,#2326,#1431,.T.);
#2874=EDGE_CURVE('',#2361,#2330,#1432,.T.);
#2875=EDGE_CURVE('',#2359,#2361,#347,.T.);
#2876=EDGE_CURVE('',#2362,#2332,#1433,.T.);
#2877=EDGE_CURVE('',#2361,#2362,#1434,.T.);
#2878=EDGE_CURVE('',#2363,#2334,#1435,.T.);
#2879=EDGE_CURVE('',#2362,#2363,#348,.T.);
#2880=EDGE_CURVE('',#2364,#2336,#1436,.T.);
#2881=EDGE_CURVE('',#2363,#2364,#1437,.T.);
#2882=EDGE_CURVE('',#2365,#2338,#1438,.T.);
#2883=EDGE_CURVE('',#2364,#2365,#349,.T.);
#2884=EDGE_CURVE('',#2366,#2340,#1439,.T.);
#2885=EDGE_CURVE('',#2365,#2366,#1440,.T.);
#2886=EDGE_CURVE('',#2367,#2342,#1441,.T.);
#2887=EDGE_CURVE('',#2366,#2367,#350,.T.);
#2888=EDGE_CURVE('',#2368,#2344,#1442,.T.);
#2889=EDGE_CURVE('',#2367,#2368,#1443,.T.);
#2890=EDGE_CURVE('',#2369,#2346,#1444,.T.);
#2891=EDGE_CURVE('',#2368,#2369,#351,.T.);
#2892=EDGE_CURVE('',#2370,#2348,#1445,.T.);
#2893=EDGE_CURVE('',#2369,#2370,#1446,.T.);
#2894=EDGE_CURVE('',#2371,#2350,#1447,.T.);
#2895=EDGE_CURVE('',#2370,#2371,#352,.T.);
#2896=EDGE_CURVE('',#2372,#2352,#1448,.T.);
#2897=EDGE_CURVE('',#2371,#2372,#1449,.T.);
#2898=EDGE_CURVE('',#2373,#2354,#1450,.T.);
#2899=EDGE_CURVE('',#2372,#2373,#353,.T.);
#2900=EDGE_CURVE('',#2374,#2356,#1451,.T.);
#2901=EDGE_CURVE('',#2373,#2374,#1452,.T.);
#2902=EDGE_CURVE('',#2358,#2375,#1453,.T.);
#2903=EDGE_CURVE('',#2374,#2375,#354,.T.);
#2904=EDGE_CURVE('',#2376,#2289,#1454,.T.);
#2905=EDGE_CURVE('',#2375,#2376,#355,.T.);
#2906=EDGE_CURVE('',#2377,#2292,#1455,.T.);
#2907=EDGE_CURVE('',#2376,#2377,#356,.T.);
#2908=EDGE_CURVE('',#2378,#2378,#357,.T.);
#2909=EDGE_CURVE('',#2379,#2379,#358,.T.);
#2910=EDGE_CURVE('',#2380,#2380,#359,.T.);
#2911=EDGE_CURVE('',#2381,#2381,#360,.T.);
#2912=EDGE_CURVE('',#2382,#2382,#361,.T.);
#2913=EDGE_CURVE('',#2376,#2383,#174,.T.);
#2914=EDGE_CURVE('',#2383,#2384,#362,.T.);
#2915=EDGE_CURVE('',#2384,#2375,#1456,.T.);
#2916=EDGE_CURVE('',#2385,#2374,#1457,.T.);
#2917=EDGE_CURVE('',#2384,#2385,#363,.T.);
#2918=EDGE_CURVE('',#2386,#2373,#1458,.T.);
#2919=EDGE_CURVE('',#2385,#2386,#1459,.T.);
#2920=EDGE_CURVE('',#2387,#2372,#1460,.T.);
#2921=EDGE_CURVE('',#2386,#2387,#364,.T.);
#2922=EDGE_CURVE('',#2387,#2388,#1461,.T.);
#2923=EDGE_CURVE('',#2388,#2371,#1462,.T.);
#2924=EDGE_CURVE('',#2389,#2370,#1463,.T.);
#2925=EDGE_CURVE('',#2388,#2389,#365,.T.);
#2926=EDGE_CURVE('',#2389,#2390,#1464,.T.);
#2927=EDGE_CURVE('',#2390,#2369,#1465,.T.);
#2928=EDGE_CURVE('',#2391,#2368,#1466,.T.);
#2929=EDGE_CURVE('',#2390,#2391,#366,.T.);
#2930=EDGE_CURVE('',#2391,#2392,#1467,.T.);
#2931=EDGE_CURVE('',#2392,#2367,#1468,.T.);
#2932=EDGE_CURVE('',#2393,#2366,#1469,.T.);
#2933=EDGE_CURVE('',#2392,#2393,#367,.T.);
#2934=EDGE_CURVE('',#2393,#2394,#1470,.T.);
#2935=EDGE_CURVE('',#2394,#2365,#1471,.T.);
#2936=EDGE_CURVE('',#2395,#2364,#1472,.T.);
#2937=EDGE_CURVE('',#2394,#2395,#368,.T.);
#2938=EDGE_CURVE('',#2395,#2396,#1473,.T.);
#2939=EDGE_CURVE('',#2396,#2363,#1474,.T.);
#2940=EDGE_CURVE('',#2397,#2362,#1475,.T.);
#2941=EDGE_CURVE('',#2396,#2397,#369,.T.);
#2942=EDGE_CURVE('',#2398,#2361,#1476,.T.);
#2943=EDGE_CURVE('',#2397,#2398,#1477,.T.);
#2944=EDGE_CURVE('',#2399,#2359,#1478,.T.);
#2945=EDGE_CURVE('',#2398,#2399,#370,.T.);
#2946=EDGE_CURVE('',#2400,#2360,#1479,.T.);
#2947=EDGE_CURVE('',#2399,#2400,#1480,.T.);
#2948=EDGE_CURVE('',#2401,#2402,#1481,.T.);
#2949=EDGE_CURVE('',#2402,#2360,#371,.T.);
#2950=EDGE_CURVE('',#2400,#2401,#372,.T.);
#2951=EDGE_CURVE('',#2401,#2403,#1482,.T.);
#2952=EDGE_CURVE('',#2403,#2404,#1483,.T.);
#2953=EDGE_CURVE('',#2404,#2402,#1484,.T.);
#2954=EDGE_CURVE('',#2403,#2405,#373,.T.);
#2955=EDGE_CURVE('',#2405,#2406,#1485,.T.);
#2956=EDGE_CURVE('',#2406,#2404,#374,.T.);
#2957=EDGE_CURVE('',#2405,#2407,#1486,.T.);
#2958=EDGE_CURVE('',#2407,#2408,#1487,.T.);
#2959=EDGE_CURVE('',#2408,#2406,#1488,.T.);
#2960=EDGE_CURVE('',#2407,#2409,#375,.T.);
#2961=EDGE_CURVE('',#2409,#2410,#1489,.T.);
#2962=EDGE_CURVE('',#2410,#2408,#376,.T.);
#2963=EDGE_CURVE('',#2411,#2412,#1490,.T.);
#2964=EDGE_CURVE('',#2412,#2410,#1491,.T.);
#2965=EDGE_CURVE('',#2409,#2411,#1492,.T.);
#2966=EDGE_CURVE('',#2411,#2413,#377,.T.);
#2967=EDGE_CURVE('',#2413,#2414,#1493,.T.);
#2968=EDGE_CURVE('',#2414,#2412,#378,.T.);
#2969=EDGE_CURVE('',#2415,#2416,#1494,.T.);
#2970=EDGE_CURVE('',#2416,#2414,#1495,.T.);
#2971=EDGE_CURVE('',#2413,#2415,#1496,.T.);
#2972=EDGE_CURVE('',#2415,#2417,#379,.T.);
#2973=EDGE_CURVE('',#2417,#2418,#1497,.T.);
#2974=EDGE_CURVE('',#2418,#2416,#380,.T.);
#2975=EDGE_CURVE('',#2419,#2420,#1498,.T.);
#2976=EDGE_CURVE('',#2420,#2418,#1499,.T.);
#2977=EDGE_CURVE('',#2417,#2419,#1500,.T.);
#2978=EDGE_CURVE('',#2419,#2421,#381,.T.);
#2979=EDGE_CURVE('',#2421,#2422,#1501,.T.);
#2980=EDGE_CURVE('',#2422,#2420,#382,.T.);
#2981=EDGE_CURVE('',#2423,#2424,#1502,.T.);
#2982=EDGE_CURVE('',#2424,#2422,#1503,.T.);
#2983=EDGE_CURVE('',#2421,#2423,#1504,.T.);
#2984=EDGE_CURVE('',#2423,#2425,#383,.T.);
#2985=EDGE_CURVE('',#2425,#2426,#1505,.T.);
#2986=EDGE_CURVE('',#2426,#2424,#384,.T.);
#2987=EDGE_CURVE('',#2427,#2428,#1506,.T.);
#2988=EDGE_CURVE('',#2428,#2426,#1507,.T.);
#2989=EDGE_CURVE('',#2425,#2427,#1508,.T.);
#2990=EDGE_CURVE('',#2427,#2429,#385,.T.);
#2991=EDGE_CURVE('',#2429,#2430,#1509,.T.);
#2992=EDGE_CURVE('',#2430,#2428,#386,.T.);
#2993=EDGE_CURVE('',#2429,#2431,#1510,.T.);
#2994=EDGE_CURVE('',#2431,#2432,#1511,.T.);
#2995=EDGE_CURVE('',#2432,#2430,#1512,.T.);
#2996=EDGE_CURVE('',#2433,#2377,#1513,.T.);
#2997=EDGE_CURVE('',#2377,#2432,#387,.T.);
#2998=EDGE_CURVE('',#2431,#2433,#388,.T.);
#2999=EDGE_CURVE('',#2433,#2383,#389,.T.);
#3000=EDGE_CURVE('',#2402,#2324,#1514,.T.);
#3001=EDGE_CURVE('',#2404,#2322,#1515,.T.);
#3002=EDGE_CURVE('',#2406,#2320,#1516,.T.);
#3003=EDGE_CURVE('',#2408,#2318,#1517,.T.);
#3004=EDGE_CURVE('',#2410,#2316,#1518,.T.);
#3005=EDGE_CURVE('',#2412,#2314,#1519,.T.);
#3006=EDGE_CURVE('',#2414,#2312,#1520,.T.);
#3007=EDGE_CURVE('',#2416,#2310,#1521,.T.);
#3008=EDGE_CURVE('',#2418,#2308,#1522,.T.);
#3009=EDGE_CURVE('',#2420,#2306,#1523,.T.);
#3010=EDGE_CURVE('',#2422,#2304,#1524,.T.);
#3011=EDGE_CURVE('',#2424,#2302,#1525,.T.);
#3012=EDGE_CURVE('',#2426,#2300,#1526,.T.);
#3013=EDGE_CURVE('',#2428,#2298,#1527,.T.);
#3014=EDGE_CURVE('',#2430,#2296,#1528,.T.);
#3015=EDGE_CURVE('',#2294,#2432,#1529,.T.);
#3016=EDGE_CURVE('',#2434,#2434,#390,.T.);
#3017=EDGE_CURVE('',#2435,#2435,#391,.T.);
#3018=EDGE_CURVE('',#2436,#2436,#392,.T.);
#3019=EDGE_CURVE('',#2437,#2437,#393,.T.);
#3020=EDGE_CURVE('',#2438,#2438,#394,.T.);
#3021=EDGE_CURVE('',#2439,#2439,#395,.T.);
#3022=EDGE_CURVE('',#2439,#2378,#1530,.T.);
#3023=EDGE_CURVE('',#2439,#2435,#1531,.T.);
#3024=EDGE_CURVE('',#2440,#2440,#396,.T.);
#3025=EDGE_CURVE('',#2440,#2382,#1532,.T.);
#3026=EDGE_CURVE('',#2440,#2436,#1533,.T.);
#3027=EDGE_CURVE('',#2379,#2441,#1534,.T.);
#3028=EDGE_CURVE('',#2441,#2441,#397,.T.);
#3029=EDGE_CURVE('',#2441,#2434,#1535,.T.);
#3030=EDGE_CURVE('',#2380,#2437,#1536,.T.);
#3031=EDGE_CURVE('',#2381,#2438,#1537,.T.);
#3398=ORIENTED_EDGE('',*,*,#2664,.F.);
#3399=ORIENTED_EDGE('',*,*,#2665,.T.);
#3400=ORIENTED_EDGE('',*,*,#2666,.T.);
#3401=ORIENTED_EDGE('',*,*,#2667,.F.);
#3402=ORIENTED_EDGE('',*,*,#2668,.F.);
#3403=ORIENTED_EDGE('',*,*,#2669,.T.);
#3404=ORIENTED_EDGE('',*,*,#2670,.T.);
#3405=ORIENTED_EDGE('',*,*,#2665,.F.);
#3406=ORIENTED_EDGE('',*,*,#2671,.F.);
#3407=ORIENTED_EDGE('',*,*,#2672,.T.);
#3408=ORIENTED_EDGE('',*,*,#2673,.T.);
#3409=ORIENTED_EDGE('',*,*,#2669,.F.);
#3410=ORIENTED_EDGE('',*,*,#2674,.F.);
#3411=ORIENTED_EDGE('',*,*,#2675,.T.);
#3412=ORIENTED_EDGE('',*,*,#2676,.T.);
#3413=ORIENTED_EDGE('',*,*,#2672,.F.);
#3414=ORIENTED_EDGE('',*,*,#2677,.F.);
#3415=ORIENTED_EDGE('',*,*,#2678,.T.);
#3416=ORIENTED_EDGE('',*,*,#2679,.T.);
#3417=ORIENTED_EDGE('',*,*,#2675,.F.);
#3418=ORIENTED_EDGE('',*,*,#2680,.F.);
#3419=ORIENTED_EDGE('',*,*,#2681,.T.);
#3420=ORIENTED_EDGE('',*,*,#2682,.T.);
#3421=ORIENTED_EDGE('',*,*,#2678,.F.);
#3422=ORIENTED_EDGE('',*,*,#2683,.F.);
#3423=ORIENTED_EDGE('',*,*,#2684,.T.);
#3424=ORIENTED_EDGE('',*,*,#2685,.T.);
#3425=ORIENTED_EDGE('',*,*,#2681,.F.);
#3426=ORIENTED_EDGE('',*,*,#2686,.F.);
#3427=ORIENTED_EDGE('',*,*,#2667,.T.);
#3428=ORIENTED_EDGE('',*,*,#2687,.T.);
#3429=ORIENTED_EDGE('',*,*,#2684,.F.);
#3430=ORIENTED_EDGE('',*,*,#2688,.F.);
#3431=ORIENTED_EDGE('',*,*,#2689,.T.);
#3432=ORIENTED_EDGE('',*,*,#2690,.T.);
#3433=ORIENTED_EDGE('',*,*,#2691,.F.);
#3434=ORIENTED_EDGE('',*,*,#2692,.F.);
#3435=ORIENTED_EDGE('',*,*,#2693,.T.);
#3436=ORIENTED_EDGE('',*,*,#2694,.T.);
#3437=ORIENTED_EDGE('',*,*,#2689,.F.);
#3438=ORIENTED_EDGE('',*,*,#2695,.F.);
#3439=ORIENTED_EDGE('',*,*,#2696,.T.);
#3440=ORIENTED_EDGE('',*,*,#2697,.T.);
#3441=ORIENTED_EDGE('',*,*,#2693,.F.);
#3442=ORIENTED_EDGE('',*,*,#2698,.F.);
#3443=ORIENTED_EDGE('',*,*,#2699,.T.);
#3444=ORIENTED_EDGE('',*,*,#2700,.T.);
#3445=ORIENTED_EDGE('',*,*,#2696,.F.);
#3446=ORIENTED_EDGE('',*,*,#2701,.F.);
#3447=ORIENTED_EDGE('',*,*,#2702,.T.);
#3448=ORIENTED_EDGE('',*,*,#2703,.T.);
#3449=ORIENTED_EDGE('',*,*,#2699,.F.);
#3450=ORIENTED_EDGE('',*,*,#2704,.F.);
#3451=ORIENTED_EDGE('',*,*,#2705,.T.);
#3452=ORIENTED_EDGE('',*,*,#2706,.T.);
#3453=ORIENTED_EDGE('',*,*,#2702,.F.);
#3454=ORIENTED_EDGE('',*,*,#2707,.F.);
#3455=ORIENTED_EDGE('',*,*,#2708,.T.);
#3456=ORIENTED_EDGE('',*,*,#2709,.T.);
#3457=ORIENTED_EDGE('',*,*,#2705,.F.);
#3458=ORIENTED_EDGE('',*,*,#2710,.F.);
#3459=ORIENTED_EDGE('',*,*,#2691,.T.);
#3460=ORIENTED_EDGE('',*,*,#2711,.T.);
#3461=ORIENTED_EDGE('',*,*,#2708,.F.);
#3462=ORIENTED_EDGE('',*,*,#2712,.F.);
#3463=ORIENTED_EDGE('',*,*,#2713,.T.);
#3464=ORIENTED_EDGE('',*,*,#2714,.T.);
#3465=ORIENTED_EDGE('',*,*,#2715,.F.);
#3466=ORIENTED_EDGE('',*,*,#2716,.F.);
#3467=ORIENTED_EDGE('',*,*,#2717,.T.);
#3468=ORIENTED_EDGE('',*,*,#2718,.T.);
#3469=ORIENTED_EDGE('',*,*,#2713,.F.);
#3470=ORIENTED_EDGE('',*,*,#2719,.F.);
#3471=ORIENTED_EDGE('',*,*,#2720,.T.);
#3472=ORIENTED_EDGE('',*,*,#2721,.T.);
#3473=ORIENTED_EDGE('',*,*,#2717,.F.);
#3474=ORIENTED_EDGE('',*,*,#2722,.F.);
#3475=ORIENTED_EDGE('',*,*,#2723,.T.);
#3476=ORIENTED_EDGE('',*,*,#2724,.T.);
#3477=ORIENTED_EDGE('',*,*,#2720,.F.);
#3478=ORIENTED_EDGE('',*,*,#2725,.F.);
#3479=ORIENTED_EDGE('',*,*,#2726,.T.);
#3480=ORIENTED_EDGE('',*,*,#2727,.T.);
#3481=ORIENTED_EDGE('',*,*,#2723,.F.);
#3482=ORIENTED_EDGE('',*,*,#2728,.F.);
#3483=ORIENTED_EDGE('',*,*,#2729,.T.);
#3484=ORIENTED_EDGE('',*,*,#2730,.T.);
#3485=ORIENTED_EDGE('',*,*,#2726,.F.);
#3486=ORIENTED_EDGE('',*,*,#2731,.F.);
#3487=ORIENTED_EDGE('',*,*,#2732,.T.);
#3488=ORIENTED_EDGE('',*,*,#2733,.T.);
#3489=ORIENTED_EDGE('',*,*,#2729,.F.);
#3490=ORIENTED_EDGE('',*,*,#2734,.F.);
#3491=ORIENTED_EDGE('',*,*,#2715,.T.);
#3492=ORIENTED_EDGE('',*,*,#2735,.T.);
#3493=ORIENTED_EDGE('',*,*,#2732,.F.);
#3494=ORIENTED_EDGE('',*,*,#2736,.F.);
#3495=ORIENTED_EDGE('',*,*,#2737,.T.);
#3496=ORIENTED_EDGE('',*,*,#2738,.T.);
#3497=ORIENTED_EDGE('',*,*,#2739,.F.);
#3498=ORIENTED_EDGE('',*,*,#2740,.F.);
#3499=ORIENTED_EDGE('',*,*,#2741,.T.);
#3500=ORIENTED_EDGE('',*,*,#2742,.T.);
#3501=ORIENTED_EDGE('',*,*,#2737,.F.);
#3502=ORIENTED_EDGE('',*,*,#2743,.F.);
#3503=ORIENTED_EDGE('',*,*,#2744,.T.);
#3504=ORIENTED_EDGE('',*,*,#2745,.T.);
#3505=ORIENTED_EDGE('',*,*,#2741,.F.);
#3506=ORIENTED_EDGE('',*,*,#2746,.F.);
#3507=ORIENTED_EDGE('',*,*,#2747,.T.);
#3508=ORIENTED_EDGE('',*,*,#2748,.T.);
#3509=ORIENTED_EDGE('',*,*,#2744,.F.);
#3510=ORIENTED_EDGE('',*,*,#2749,.F.);
#3511=ORIENTED_EDGE('',*,*,#2750,.T.);
#3512=ORIENTED_EDGE('',*,*,#2751,.T.);
#3513=ORIENTED_EDGE('',*,*,#2747,.F.);
#3514=ORIENTED_EDGE('',*,*,#2752,.F.);
#3515=ORIENTED_EDGE('',*,*,#2753,.T.);
#3516=ORIENTED_EDGE('',*,*,#2754,.T.);
#3517=ORIENTED_EDGE('',*,*,#2750,.F.);
#3518=ORIENTED_EDGE('',*,*,#2755,.F.);
#3519=ORIENTED_EDGE('',*,*,#2756,.T.);
#3520=ORIENTED_EDGE('',*,*,#2757,.T.);
#3521=ORIENTED_EDGE('',*,*,#2753,.F.);
#3522=ORIENTED_EDGE('',*,*,#2758,.F.);
#3523=ORIENTED_EDGE('',*,*,#2739,.T.);
#3524=ORIENTED_EDGE('',*,*,#2759,.T.);
#3525=ORIENTED_EDGE('',*,*,#2756,.F.);
#3526=ORIENTED_EDGE('',*,*,#2760,.F.);
#3527=ORIENTED_EDGE('',*,*,#2761,.T.);
#3528=ORIENTED_EDGE('',*,*,#2762,.T.);
#3529=ORIENTED_EDGE('',*,*,#2761,.F.);
#3530=ORIENTED_EDGE('',*,*,#2763,.T.);
#3531=ORIENTED_EDGE('',*,*,#2764,.T.);
#3532=ORIENTED_EDGE('',*,*,#2765,.T.);
#3533=ORIENTED_EDGE('',*,*,#2764,.F.);
#3534=ORIENTED_EDGE('',*,*,#2766,.T.);
#3535=ORIENTED_EDGE('',*,*,#2767,.T.);
#3536=ORIENTED_EDGE('',*,*,#2768,.T.);
#3537=ORIENTED_EDGE('',*,*,#2769,.T.);
#3538=ORIENTED_EDGE('',*,*,#2770,.T.);
#3539=ORIENTED_EDGE('',*,*,#2771,.T.);
#3540=ORIENTED_EDGE('',*,*,#2768,.F.);
#3541=ORIENTED_EDGE('',*,*,#2772,.T.);
#3542=ORIENTED_EDGE('',*,*,#2773,.T.);
#3543=ORIENTED_EDGE('',*,*,#2774,.T.);
#3544=ORIENTED_EDGE('',*,*,#2770,.F.);
#3545=ORIENTED_EDGE('',*,*,#2775,.T.);
#3546=ORIENTED_EDGE('',*,*,#2776,.T.);
#3547=ORIENTED_EDGE('',*,*,#2777,.T.);
#3548=ORIENTED_EDGE('',*,*,#2773,.F.);
#3549=ORIENTED_EDGE('',*,*,#2778,.T.);
#3550=ORIENTED_EDGE('',*,*,#2779,.T.);
#3551=ORIENTED_EDGE('',*,*,#2780,.T.);
#3552=ORIENTED_EDGE('',*,*,#2776,.F.);
#3553=ORIENTED_EDGE('',*,*,#2781,.T.);
#3554=ORIENTED_EDGE('',*,*,#2782,.T.);
#3555=ORIENTED_EDGE('',*,*,#2783,.T.);
#3556=ORIENTED_EDGE('',*,*,#2779,.F.);
#3557=ORIENTED_EDGE('',*,*,#2784,.T.);
#3558=ORIENTED_EDGE('',*,*,#2785,.T.);
#3559=ORIENTED_EDGE('',*,*,#2786,.T.);
#3560=ORIENTED_EDGE('',*,*,#2782,.F.);
#3561=ORIENTED_EDGE('',*,*,#2787,.T.);
#3562=ORIENTED_EDGE('',*,*,#2788,.T.);
#3563=ORIENTED_EDGE('',*,*,#2789,.T.);
#3564=ORIENTED_EDGE('',*,*,#2785,.F.);
#3565=ORIENTED_EDGE('',*,*,#2790,.T.);
#3566=ORIENTED_EDGE('',*,*,#2791,.T.);
#3567=ORIENTED_EDGE('',*,*,#2792,.T.);
#3568=ORIENTED_EDGE('',*,*,#2788,.F.);
#3569=ORIENTED_EDGE('',*,*,#2793,.T.);
#3570=ORIENTED_EDGE('',*,*,#2794,.T.);
#3571=ORIENTED_EDGE('',*,*,#2795,.T.);
#3572=ORIENTED_EDGE('',*,*,#2791,.F.);
#3573=ORIENTED_EDGE('',*,*,#2796,.T.);
#3574=ORIENTED_EDGE('',*,*,#2797,.T.);
#3575=ORIENTED_EDGE('',*,*,#2798,.T.);
#3576=ORIENTED_EDGE('',*,*,#2794,.F.);
#3577=ORIENTED_EDGE('',*,*,#2799,.T.);
#3578=ORIENTED_EDGE('',*,*,#2800,.T.);
#3579=ORIENTED_EDGE('',*,*,#2801,.T.);
#3580=ORIENTED_EDGE('',*,*,#2797,.F.);
#3581=ORIENTED_EDGE('',*,*,#2802,.T.);
#3582=ORIENTED_EDGE('',*,*,#2803,.T.);
#3583=ORIENTED_EDGE('',*,*,#2804,.T.);
#3584=ORIENTED_EDGE('',*,*,#2800,.F.);
#3585=ORIENTED_EDGE('',*,*,#2805,.T.);
#3586=ORIENTED_EDGE('',*,*,#2806,.T.);
#3587=ORIENTED_EDGE('',*,*,#2807,.T.);
#3588=ORIENTED_EDGE('',*,*,#2803,.F.);
#3589=ORIENTED_EDGE('',*,*,#2808,.T.);
#3590=ORIENTED_EDGE('',*,*,#2809,.T.);
#3591=ORIENTED_EDGE('',*,*,#2810,.T.);
#3592=ORIENTED_EDGE('',*,*,#2806,.F.);
#3593=ORIENTED_EDGE('',*,*,#2811,.T.);
#3594=ORIENTED_EDGE('',*,*,#2812,.T.);
#3595=ORIENTED_EDGE('',*,*,#2813,.T.);
#3596=ORIENTED_EDGE('',*,*,#2809,.F.);
#3597=ORIENTED_EDGE('',*,*,#2814,.T.);
#3598=ORIENTED_EDGE('',*,*,#2815,.T.);
#3599=ORIENTED_EDGE('',*,*,#2816,.T.);
#3600=ORIENTED_EDGE('',*,*,#2812,.F.);
#3601=ORIENTED_EDGE('',*,*,#2817,.T.);
#3602=ORIENTED_EDGE('',*,*,#2815,.F.);
#3603=ORIENTED_EDGE('',*,*,#2818,.T.);
#3604=ORIENTED_EDGE('',*,*,#2819,.T.);
#3605=ORIENTED_EDGE('',*,*,#2820,.T.);
#3606=ORIENTED_EDGE('',*,*,#2819,.F.);
#3607=ORIENTED_EDGE('',*,*,#2821,.T.);
#3608=ORIENTED_EDGE('',*,*,#2822,.T.);
#3609=ORIENTED_EDGE('',*,*,#2823,.T.);
#3610=ORIENTED_EDGE('',*,*,#2822,.F.);
#3611=ORIENTED_EDGE('',*,*,#2824,.T.);
#3612=ORIENTED_EDGE('',*,*,#2825,.T.);
#3613=ORIENTED_EDGE('',*,*,#2826,.T.);
#3614=ORIENTED_EDGE('',*,*,#2825,.F.);
#3615=ORIENTED_EDGE('',*,*,#2827,.T.);
#3616=ORIENTED_EDGE('',*,*,#2828,.T.);
#3617=ORIENTED_EDGE('',*,*,#2829,.T.);
#3618=ORIENTED_EDGE('',*,*,#2828,.F.);
#3619=ORIENTED_EDGE('',*,*,#2830,.T.);
#3620=ORIENTED_EDGE('',*,*,#2831,.T.);
#3621=ORIENTED_EDGE('',*,*,#2832,.T.);
#3622=ORIENTED_EDGE('',*,*,#2831,.F.);
#3623=ORIENTED_EDGE('',*,*,#2833,.T.);
#3624=ORIENTED_EDGE('',*,*,#2834,.T.);
#3625=ORIENTED_EDGE('',*,*,#2835,.T.);
#3626=ORIENTED_EDGE('',*,*,#2834,.F.);
#3627=ORIENTED_EDGE('',*,*,#2836,.T.);
#3628=ORIENTED_EDGE('',*,*,#2837,.T.);
#3629=ORIENTED_EDGE('',*,*,#2838,.T.);
#3630=ORIENTED_EDGE('',*,*,#2837,.F.);
#3631=ORIENTED_EDGE('',*,*,#2839,.T.);
#3632=ORIENTED_EDGE('',*,*,#2840,.T.);
#3633=ORIENTED_EDGE('',*,*,#2841,.T.);
#3634=ORIENTED_EDGE('',*,*,#2840,.F.);
#3635=ORIENTED_EDGE('',*,*,#2842,.T.);
#3636=ORIENTED_EDGE('',*,*,#2843,.T.);
#3637=ORIENTED_EDGE('',*,*,#2844,.T.);
#3638=ORIENTED_EDGE('',*,*,#2843,.F.);
#3639=ORIENTED_EDGE('',*,*,#2845,.T.);
#3640=ORIENTED_EDGE('',*,*,#2846,.T.);
#3641=ORIENTED_EDGE('',*,*,#2847,.T.);
#3642=ORIENTED_EDGE('',*,*,#2846,.F.);
#3643=ORIENTED_EDGE('',*,*,#2848,.T.);
#3644=ORIENTED_EDGE('',*,*,#2849,.T.);
#3645=ORIENTED_EDGE('',*,*,#2850,.T.);
#3646=ORIENTED_EDGE('',*,*,#2849,.F.);
#3647=ORIENTED_EDGE('',*,*,#2851,.T.);
#3648=ORIENTED_EDGE('',*,*,#2852,.T.);
#3649=ORIENTED_EDGE('',*,*,#2853,.T.);
#3650=ORIENTED_EDGE('',*,*,#2852,.F.);
#3651=ORIENTED_EDGE('',*,*,#2854,.T.);
#3652=ORIENTED_EDGE('',*,*,#2855,.T.);
#3653=ORIENTED_EDGE('',*,*,#2856,.T.);
#3654=ORIENTED_EDGE('',*,*,#2855,.F.);
#3655=ORIENTED_EDGE('',*,*,#2857,.T.);
#3656=ORIENTED_EDGE('',*,*,#2858,.T.);
#3657=ORIENTED_EDGE('',*,*,#2859,.T.);
#3658=ORIENTED_EDGE('',*,*,#2858,.F.);
#3659=ORIENTED_EDGE('',*,*,#2860,.T.);
#3660=ORIENTED_EDGE('',*,*,#2861,.T.);
#3661=ORIENTED_EDGE('',*,*,#2862,.T.);
#3662=ORIENTED_EDGE('',*,*,#2861,.F.);
#3663=ORIENTED_EDGE('',*,*,#2863,.T.);
#3664=ORIENTED_EDGE('',*,*,#2864,.T.);
#3665=ORIENTED_EDGE('',*,*,#2865,.T.);
#3666=ORIENTED_EDGE('',*,*,#2866,.T.);
#3667=ORIENTED_EDGE('',*,*,#2867,.T.);
#3668=ORIENTED_EDGE('',*,*,#2864,.F.);
#3669=ORIENTED_EDGE('',*,*,#2868,.T.);
#3670=ORIENTED_EDGE('',*,*,#2766,.F.);
#3671=ORIENTED_EDGE('',*,*,#2869,.T.);
#3672=ORIENTED_EDGE('',*,*,#2866,.F.);
#3673=ORIENTED_EDGE('',*,*,#2870,.T.);
#3674=ORIENTED_EDGE('',*,*,#2823,.F.);
#3675=ORIENTED_EDGE('',*,*,#2871,.F.);
#3676=ORIENTED_EDGE('',*,*,#2872,.F.);
#3677=ORIENTED_EDGE('',*,*,#2873,.T.);
#3678=ORIENTED_EDGE('',*,*,#2826,.F.);
#3679=ORIENTED_EDGE('',*,*,#2874,.F.);
#3680=ORIENTED_EDGE('',*,*,#2875,.F.);
#3681=ORIENTED_EDGE('',*,*,#2871,.T.);
#3682=ORIENTED_EDGE('',*,*,#2829,.F.);
#3683=ORIENTED_EDGE('',*,*,#2876,.F.);
#3684=ORIENTED_EDGE('',*,*,#2877,.F.);
#3685=ORIENTED_EDGE('',*,*,#2874,.T.);
#3686=ORIENTED_EDGE('',*,*,#2832,.F.);
#3687=ORIENTED_EDGE('',*,*,#2878,.F.);
#3688=ORIENTED_EDGE('',*,*,#2879,.F.);
#3689=ORIENTED_EDGE('',*,*,#2876,.T.);
#3690=ORIENTED_EDGE('',*,*,#2835,.F.);
#3691=ORIENTED_EDGE('',*,*,#2880,.F.);
#3692=ORIENTED_EDGE('',*,*,#2881,.F.);
#3693=ORIENTED_EDGE('',*,*,#2878,.T.);
#3694=ORIENTED_EDGE('',*,*,#2838,.F.);
#3695=ORIENTED_EDGE('',*,*,#2882,.F.);
#3696=ORIENTED_EDGE('',*,*,#2883,.F.);
#3697=ORIENTED_EDGE('',*,*,#2880,.T.);
#3698=ORIENTED_EDGE('',*,*,#2841,.F.);
#3699=ORIENTED_EDGE('',*,*,#2884,.F.);
#3700=ORIENTED_EDGE('',*,*,#2885,.F.);
#3701=ORIENTED_EDGE('',*,*,#2882,.T.);
#3702=ORIENTED_EDGE('',*,*,#2844,.F.);
#3703=ORIENTED_EDGE('',*,*,#2886,.F.);
#3704=ORIENTED_EDGE('',*,*,#2887,.F.);
#3705=ORIENTED_EDGE('',*,*,#2884,.T.);
#3706=ORIENTED_EDGE('',*,*,#2847,.F.);
#3707=ORIENTED_EDGE('',*,*,#2888,.F.);
#3708=ORIENTED_EDGE('',*,*,#2889,.F.);
#3709=ORIENTED_EDGE('',*,*,#2886,.T.);
#3710=ORIENTED_EDGE('',*,*,#2850,.F.);
#3711=ORIENTED_EDGE('',*,*,#2890,.F.);
#3712=ORIENTED_EDGE('',*,*,#2891,.F.);
#3713=ORIENTED_EDGE('',*,*,#2888,.T.);
#3714=ORIENTED_EDGE('',*,*,#2853,.F.);
#3715=ORIENTED_EDGE('',*,*,#2892,.F.);
#3716=ORIENTED_EDGE('',*,*,#2893,.F.);
#3717=ORIENTED_EDGE('',*,*,#2890,.T.);
#3718=ORIENTED_EDGE('',*,*,#2856,.F.);
#3719=ORIENTED_EDGE('',*,*,#2894,.F.);
#3720=ORIENTED_EDGE('',*,*,#2895,.F.);
#3721=ORIENTED_EDGE('',*,*,#2892,.T.);
#3722=ORIENTED_EDGE('',*,*,#2859,.F.);
#3723=ORIENTED_EDGE('',*,*,#2896,.F.);
#3724=ORIENTED_EDGE('',*,*,#2897,.F.);
#3725=ORIENTED_EDGE('',*,*,#2894,.T.);
#3726=ORIENTED_EDGE('',*,*,#2862,.F.);
#3727=ORIENTED_EDGE('',*,*,#2898,.F.);
#3728=ORIENTED_EDGE('',*,*,#2899,.F.);
#3729=ORIENTED_EDGE('',*,*,#2896,.T.);
#3730=ORIENTED_EDGE('',*,*,#2865,.F.);
#3731=ORIENTED_EDGE('',*,*,#2900,.F.);
#3732=ORIENTED_EDGE('',*,*,#2901,.F.);
#3733=ORIENTED_EDGE('',*,*,#2898,.T.);
#3734=ORIENTED_EDGE('',*,*,#2867,.F.);
#3735=ORIENTED_EDGE('',*,*,#2902,.T.);
#3736=ORIENTED_EDGE('',*,*,#2903,.F.);
#3737=ORIENTED_EDGE('',*,*,#2900,.T.);
#3738=ORIENTED_EDGE('',*,*,#2869,.F.);
#3739=ORIENTED_EDGE('',*,*,#2904,.F.);
#3740=ORIENTED_EDGE('',*,*,#2905,.F.);
#3741=ORIENTED_EDGE('',*,*,#2902,.F.);
#3742=ORIENTED_EDGE('',*,*,#2769,.F.);
#3743=ORIENTED_EDGE('',*,*,#2906,.F.);
#3744=ORIENTED_EDGE('',*,*,#2907,.F.);
#3745=ORIENTED_EDGE('',*,*,#2904,.T.);
#3746=ORIENTED_EDGE('',*,*,#2767,.F.);
#3747=ORIENTED_EDGE('',*,*,#2870,.F.);
#3748=ORIENTED_EDGE('',*,*,#2868,.F.);
#3749=ORIENTED_EDGE('',*,*,#2863,.F.);
#3750=ORIENTED_EDGE('',*,*,#2860,.F.);
#3751=ORIENTED_EDGE('',*,*,#2857,.F.);
#3752=ORIENTED_EDGE('',*,*,#2854,.F.);
#3753=ORIENTED_EDGE('',*,*,#2851,.F.);
#3754=ORIENTED_EDGE('',*,*,#2848,.F.);
#3755=ORIENTED_EDGE('',*,*,#2845,.F.);
#3756=ORIENTED_EDGE('',*,*,#2842,.F.);
#3757=ORIENTED_EDGE('',*,*,#2839,.F.);
#3758=ORIENTED_EDGE('',*,*,#2836,.F.);
#3759=ORIENTED_EDGE('',*,*,#2833,.F.);
#3760=ORIENTED_EDGE('',*,*,#2830,.F.);
#3761=ORIENTED_EDGE('',*,*,#2827,.F.);
#3762=ORIENTED_EDGE('',*,*,#2824,.F.);
#3763=ORIENTED_EDGE('',*,*,#2821,.F.);
#3764=ORIENTED_EDGE('',*,*,#2818,.F.);
#3765=ORIENTED_EDGE('',*,*,#2817,.F.);
#3766=ORIENTED_EDGE('',*,*,#2814,.F.);
#3767=ORIENTED_EDGE('',*,*,#2811,.F.);
#3768=ORIENTED_EDGE('',*,*,#2808,.F.);
#3769=ORIENTED_EDGE('',*,*,#2805,.F.);
#3770=ORIENTED_EDGE('',*,*,#2802,.F.);
#3771=ORIENTED_EDGE('',*,*,#2799,.F.);
#3772=ORIENTED_EDGE('',*,*,#2796,.F.);
#3773=ORIENTED_EDGE('',*,*,#2793,.F.);
#3774=ORIENTED_EDGE('',*,*,#2790,.F.);
#3775=ORIENTED_EDGE('',*,*,#2787,.F.);
#3776=ORIENTED_EDGE('',*,*,#2784,.F.);
#3777=ORIENTED_EDGE('',*,*,#2781,.F.);
#3778=ORIENTED_EDGE('',*,*,#2778,.F.);
#3779=ORIENTED_EDGE('',*,*,#2775,.F.);
#3780=ORIENTED_EDGE('',*,*,#2772,.F.);
#3781=ORIENTED_EDGE('',*,*,#2908,.F.);
#3782=ORIENTED_EDGE('',*,*,#2909,.F.);
#3783=ORIENTED_EDGE('',*,*,#2910,.F.);
#3784=ORIENTED_EDGE('',*,*,#2763,.F.);
#3785=ORIENTED_EDGE('',*,*,#2911,.T.);
#3786=ORIENTED_EDGE('',*,*,#2760,.T.);
#3787=ORIENTED_EDGE('',*,*,#2912,.F.);
#3788=ORIENTED_EDGE('',*,*,#2913,.T.);
#3789=ORIENTED_EDGE('',*,*,#2914,.T.);
#3790=ORIENTED_EDGE('',*,*,#2915,.T.);
#3791=ORIENTED_EDGE('',*,*,#2905,.T.);
#3792=ORIENTED_EDGE('',*,*,#2916,.T.);
#3793=ORIENTED_EDGE('',*,*,#2903,.T.);
#3794=ORIENTED_EDGE('',*,*,#2915,.F.);
#3795=ORIENTED_EDGE('',*,*,#2917,.T.);
#3796=ORIENTED_EDGE('',*,*,#2918,.T.);
#3797=ORIENTED_EDGE('',*,*,#2901,.T.);
#3798=ORIENTED_EDGE('',*,*,#2916,.F.);
#3799=ORIENTED_EDGE('',*,*,#2919,.T.);
#3800=ORIENTED_EDGE('',*,*,#2920,.T.);
#3801=ORIENTED_EDGE('',*,*,#2899,.T.);
#3802=ORIENTED_EDGE('',*,*,#2918,.F.);
#3803=ORIENTED_EDGE('',*,*,#2921,.T.);
#3804=ORIENTED_EDGE('',*,*,#2920,.F.);
#3805=ORIENTED_EDGE('',*,*,#2922,.T.);
#3806=ORIENTED_EDGE('',*,*,#2923,.T.);
#3807=ORIENTED_EDGE('',*,*,#2897,.T.);
#3808=ORIENTED_EDGE('',*,*,#2924,.T.);
#3809=ORIENTED_EDGE('',*,*,#2895,.T.);
#3810=ORIENTED_EDGE('',*,*,#2923,.F.);
#3811=ORIENTED_EDGE('',*,*,#2925,.T.);
#3812=ORIENTED_EDGE('',*,*,#2924,.F.);
#3813=ORIENTED_EDGE('',*,*,#2926,.T.);
#3814=ORIENTED_EDGE('',*,*,#2927,.T.);
#3815=ORIENTED_EDGE('',*,*,#2893,.T.);
#3816=ORIENTED_EDGE('',*,*,#2928,.T.);
#3817=ORIENTED_EDGE('',*,*,#2891,.T.);
#3818=ORIENTED_EDGE('',*,*,#2927,.F.);
#3819=ORIENTED_EDGE('',*,*,#2929,.T.);
#3820=ORIENTED_EDGE('',*,*,#2928,.F.);
#3821=ORIENTED_EDGE('',*,*,#2930,.T.);
#3822=ORIENTED_EDGE('',*,*,#2931,.T.);
#3823=ORIENTED_EDGE('',*,*,#2889,.T.);
#3824=ORIENTED_EDGE('',*,*,#2932,.T.);
#3825=ORIENTED_EDGE('',*,*,#2887,.T.);
#3826=ORIENTED_EDGE('',*,*,#2931,.F.);
#3827=ORIENTED_EDGE('',*,*,#2933,.T.);
#3828=ORIENTED_EDGE('',*,*,#2932,.F.);
#3829=ORIENTED_EDGE('',*,*,#2934,.T.);
#3830=ORIENTED_EDGE('',*,*,#2935,.T.);
#3831=ORIENTED_EDGE('',*,*,#2885,.T.);
#3832=ORIENTED_EDGE('',*,*,#2936,.T.);
#3833=ORIENTED_EDGE('',*,*,#2883,.T.);
#3834=ORIENTED_EDGE('',*,*,#2935,.F.);
#3835=ORIENTED_EDGE('',*,*,#2937,.T.);
#3836=ORIENTED_EDGE('',*,*,#2936,.F.);
#3837=ORIENTED_EDGE('',*,*,#2938,.T.);
#3838=ORIENTED_EDGE('',*,*,#2939,.T.);
#3839=ORIENTED_EDGE('',*,*,#2881,.T.);
#3840=ORIENTED_EDGE('',*,*,#2940,.T.);
#3841=ORIENTED_EDGE('',*,*,#2879,.T.);
#3842=ORIENTED_EDGE('',*,*,#2939,.F.);
#3843=ORIENTED_EDGE('',*,*,#2941,.T.);
#3844=ORIENTED_EDGE('',*,*,#2942,.T.);
#3845=ORIENTED_EDGE('',*,*,#2877,.T.);
#3846=ORIENTED_EDGE('',*,*,#2940,.F.);
#3847=ORIENTED_EDGE('',*,*,#2943,.T.);
#3848=ORIENTED_EDGE('',*,*,#2944,.T.);
#3849=ORIENTED_EDGE('',*,*,#2875,.T.);
#3850=ORIENTED_EDGE('',*,*,#2942,.F.);
#3851=ORIENTED_EDGE('',*,*,#2945,.T.);
#3852=ORIENTED_EDGE('',*,*,#2946,.T.);
#3853=ORIENTED_EDGE('',*,*,#2872,.T.);
#3854=ORIENTED_EDGE('',*,*,#2944,.F.);
#3855=ORIENTED_EDGE('',*,*,#2947,.T.);
#3856=ORIENTED_EDGE('',*,*,#2948,.T.);
#3857=ORIENTED_EDGE('',*,*,#2949,.T.);
#3858=ORIENTED_EDGE('',*,*,#2946,.F.);
#3859=ORIENTED_EDGE('',*,*,#2950,.T.);
#3860=ORIENTED_EDGE('',*,*,#2948,.F.);
#3861=ORIENTED_EDGE('',*,*,#2951,.T.);
#3862=ORIENTED_EDGE('',*,*,#2952,.T.);
#3863=ORIENTED_EDGE('',*,*,#2953,.T.);
#3864=ORIENTED_EDGE('',*,*,#2952,.F.);
#3865=ORIENTED_EDGE('',*,*,#2954,.T.);
#3866=ORIENTED_EDGE('',*,*,#2955,.T.);
#3867=ORIENTED_EDGE('',*,*,#2956,.T.);
#3868=ORIENTED_EDGE('',*,*,#2955,.F.);
#3869=ORIENTED_EDGE('',*,*,#2957,.T.);
#3870=ORIENTED_EDGE('',*,*,#2958,.T.);
#3871=ORIENTED_EDGE('',*,*,#2959,.T.);
#3872=ORIENTED_EDGE('',*,*,#2958,.F.);
#3873=ORIENTED_EDGE('',*,*,#2960,.T.);
#3874=ORIENTED_EDGE('',*,*,#2961,.T.);
#3875=ORIENTED_EDGE('',*,*,#2962,.T.);
#3876=ORIENTED_EDGE('',*,*,#2963,.T.);
#3877=ORIENTED_EDGE('',*,*,#2964,.T.);
#3878=ORIENTED_EDGE('',*,*,#2961,.F.);
#3879=ORIENTED_EDGE('',*,*,#2965,.T.);
#3880=ORIENTED_EDGE('',*,*,#2963,.F.);
#3881=ORIENTED_EDGE('',*,*,#2966,.T.);
#3882=ORIENTED_EDGE('',*,*,#2967,.T.);
#3883=ORIENTED_EDGE('',*,*,#2968,.T.);
#3884=ORIENTED_EDGE('',*,*,#2969,.T.);
#3885=ORIENTED_EDGE('',*,*,#2970,.T.);
#3886=ORIENTED_EDGE('',*,*,#2967,.F.);
#3887=ORIENTED_EDGE('',*,*,#2971,.T.);
#3888=ORIENTED_EDGE('',*,*,#2969,.F.);
#3889=ORIENTED_EDGE('',*,*,#2972,.T.);
#3890=ORIENTED_EDGE('',*,*,#2973,.T.);
#3891=ORIENTED_EDGE('',*,*,#2974,.T.);
#3892=ORIENTED_EDGE('',*,*,#2975,.T.);
#3893=ORIENTED_EDGE('',*,*,#2976,.T.);
#3894=ORIENTED_EDGE('',*,*,#2973,.F.);
#3895=ORIENTED_EDGE('',*,*,#2977,.T.);
#3896=ORIENTED_EDGE('',*,*,#2975,.F.);
#3897=ORIENTED_EDGE('',*,*,#2978,.T.);
#3898=ORIENTED_EDGE('',*,*,#2979,.T.);
#3899=ORIENTED_EDGE('',*,*,#2980,.T.);
#3900=ORIENTED_EDGE('',*,*,#2981,.T.);
#3901=ORIENTED_EDGE('',*,*,#2982,.T.);
#3902=ORIENTED_EDGE('',*,*,#2979,.F.);
#3903=ORIENTED_EDGE('',*,*,#2983,.T.);
#3904=ORIENTED_EDGE('',*,*,#2981,.F.);
#3905=ORIENTED_EDGE('',*,*,#2984,.T.);
#3906=ORIENTED_EDGE('',*,*,#2985,.T.);
#3907=ORIENTED_EDGE('',*,*,#2986,.T.);
#3908=ORIENTED_EDGE('',*,*,#2987,.T.);
#3909=ORIENTED_EDGE('',*,*,#2988,.T.);
#3910=ORIENTED_EDGE('',*,*,#2985,.F.);
#3911=ORIENTED_EDGE('',*,*,#2989,.T.);
#3912=ORIENTED_EDGE('',*,*,#2987,.F.);
#3913=ORIENTED_EDGE('',*,*,#2990,.T.);
#3914=ORIENTED_EDGE('',*,*,#2991,.T.);
#3915=ORIENTED_EDGE('',*,*,#2992,.T.);
#3916=ORIENTED_EDGE('',*,*,#2991,.F.);
#3917=ORIENTED_EDGE('',*,*,#2993,.T.);
#3918=ORIENTED_EDGE('',*,*,#2994,.T.);
#3919=ORIENTED_EDGE('',*,*,#2995,.T.);
#3920=ORIENTED_EDGE('',*,*,#2996,.T.);
#3921=ORIENTED_EDGE('',*,*,#2997,.T.);
#3922=ORIENTED_EDGE('',*,*,#2994,.F.);
#3923=ORIENTED_EDGE('',*,*,#2998,.T.);
#3924=ORIENTED_EDGE('',*,*,#2913,.F.);
#3925=ORIENTED_EDGE('',*,*,#2907,.T.);
#3926=ORIENTED_EDGE('',*,*,#2996,.F.);
#3927=ORIENTED_EDGE('',*,*,#2999,.T.);
#3928=ORIENTED_EDGE('',*,*,#2816,.F.);
#3929=ORIENTED_EDGE('',*,*,#3000,.F.);
#3930=ORIENTED_EDGE('',*,*,#2953,.F.);
#3931=ORIENTED_EDGE('',*,*,#3001,.T.);
#3932=ORIENTED_EDGE('',*,*,#2813,.F.);
#3933=ORIENTED_EDGE('',*,*,#3001,.F.);
#3934=ORIENTED_EDGE('',*,*,#2956,.F.);
#3935=ORIENTED_EDGE('',*,*,#3002,.T.);
#3936=ORIENTED_EDGE('',*,*,#2810,.F.);
#3937=ORIENTED_EDGE('',*,*,#3002,.F.);
#3938=ORIENTED_EDGE('',*,*,#2959,.F.);
#3939=ORIENTED_EDGE('',*,*,#3003,.T.);
#3940=ORIENTED_EDGE('',*,*,#2807,.F.);
#3941=ORIENTED_EDGE('',*,*,#3003,.F.);
#3942=ORIENTED_EDGE('',*,*,#2962,.F.);
#3943=ORIENTED_EDGE('',*,*,#3004,.T.);
#3944=ORIENTED_EDGE('',*,*,#2804,.F.);
#3945=ORIENTED_EDGE('',*,*,#3004,.F.);
#3946=ORIENTED_EDGE('',*,*,#2964,.F.);
#3947=ORIENTED_EDGE('',*,*,#3005,.T.);
#3948=ORIENTED_EDGE('',*,*,#2801,.F.);
#3949=ORIENTED_EDGE('',*,*,#3005,.F.);
#3950=ORIENTED_EDGE('',*,*,#2968,.F.);
#3951=ORIENTED_EDGE('',*,*,#3006,.T.);
#3952=ORIENTED_EDGE('',*,*,#2798,.F.);
#3953=ORIENTED_EDGE('',*,*,#3006,.F.);
#3954=ORIENTED_EDGE('',*,*,#2970,.F.);
#3955=ORIENTED_EDGE('',*,*,#3007,.T.);
#3956=ORIENTED_EDGE('',*,*,#2795,.F.);
#3957=ORIENTED_EDGE('',*,*,#3007,.F.);
#3958=ORIENTED_EDGE('',*,*,#2974,.F.);
#3959=ORIENTED_EDGE('',*,*,#3008,.T.);
#3960=ORIENTED_EDGE('',*,*,#2792,.F.);
#3961=ORIENTED_EDGE('',*,*,#3008,.F.);
#3962=ORIENTED_EDGE('',*,*,#2976,.F.);
#3963=ORIENTED_EDGE('',*,*,#3009,.T.);
#3964=ORIENTED_EDGE('',*,*,#2789,.F.);
#3965=ORIENTED_EDGE('',*,*,#3009,.F.);
#3966=ORIENTED_EDGE('',*,*,#2980,.F.);
#3967=ORIENTED_EDGE('',*,*,#3010,.T.);
#3968=ORIENTED_EDGE('',*,*,#2786,.F.);
#3969=ORIENTED_EDGE('',*,*,#3010,.F.);
#3970=ORIENTED_EDGE('',*,*,#2982,.F.);
#3971=ORIENTED_EDGE('',*,*,#3011,.T.);
#3972=ORIENTED_EDGE('',*,*,#2783,.F.);
#3973=ORIENTED_EDGE('',*,*,#3011,.F.);
#3974=ORIENTED_EDGE('',*,*,#2986,.F.);
#3975=ORIENTED_EDGE('',*,*,#3012,.T.);
#3976=ORIENTED_EDGE('',*,*,#2780,.F.);
#3977=ORIENTED_EDGE('',*,*,#3012,.F.);
#3978=ORIENTED_EDGE('',*,*,#2988,.F.);
#3979=ORIENTED_EDGE('',*,*,#3013,.T.);
#3980=ORIENTED_EDGE('',*,*,#2777,.F.);
#3981=ORIENTED_EDGE('',*,*,#3013,.F.);
#3982=ORIENTED_EDGE('',*,*,#2992,.F.);
#3983=ORIENTED_EDGE('',*,*,#3014,.T.);
#3984=ORIENTED_EDGE('',*,*,#2774,.F.);
#3985=ORIENTED_EDGE('',*,*,#3014,.F.);
#3986=ORIENTED_EDGE('',*,*,#2995,.F.);
#3987=ORIENTED_EDGE('',*,*,#3015,.F.);
#3988=ORIENTED_EDGE('',*,*,#2771,.F.);
#3989=ORIENTED_EDGE('',*,*,#3015,.T.);
#3990=ORIENTED_EDGE('',*,*,#2997,.F.);
#3991=ORIENTED_EDGE('',*,*,#2906,.T.);
#3992=ORIENTED_EDGE('',*,*,#2914,.F.);
#3993=ORIENTED_EDGE('',*,*,#2999,.F.);
#3994=ORIENTED_EDGE('',*,*,#2998,.F.);
#3995=ORIENTED_EDGE('',*,*,#2993,.F.);
#3996=ORIENTED_EDGE('',*,*,#2990,.F.);
#3997=ORIENTED_EDGE('',*,*,#2989,.F.);
#3998=ORIENTED_EDGE('',*,*,#2984,.F.);
#3999=ORIENTED_EDGE('',*,*,#2983,.F.);
#4000=ORIENTED_EDGE('',*,*,#2978,.F.);
#4001=ORIENTED_EDGE('',*,*,#2977,.F.);
#4002=ORIENTED_EDGE('',*,*,#2972,.F.);
#4003=ORIENTED_EDGE('',*,*,#2971,.F.);
#4004=ORIENTED_EDGE('',*,*,#2966,.F.);
#4005=ORIENTED_EDGE('',*,*,#2965,.F.);
#4006=ORIENTED_EDGE('',*,*,#2960,.F.);
#4007=ORIENTED_EDGE('',*,*,#2957,.F.);
#4008=ORIENTED_EDGE('',*,*,#2954,.F.);
#4009=ORIENTED_EDGE('',*,*,#2951,.F.);
#4010=ORIENTED_EDGE('',*,*,#2950,.F.);
#4011=ORIENTED_EDGE('',*,*,#2947,.F.);
#4012=ORIENTED_EDGE('',*,*,#2945,.F.);
#4013=ORIENTED_EDGE('',*,*,#2943,.F.);
#4014=ORIENTED_EDGE('',*,*,#2941,.F.);
#4015=ORIENTED_EDGE('',*,*,#2938,.F.);
#4016=ORIENTED_EDGE('',*,*,#2937,.F.);
#4017=ORIENTED_EDGE('',*,*,#2934,.F.);
#4018=ORIENTED_EDGE('',*,*,#2933,.F.);
#4019=ORIENTED_EDGE('',*,*,#2930,.F.);
#4020=ORIENTED_EDGE('',*,*,#2929,.F.);
#4021=ORIENTED_EDGE('',*,*,#2926,.F.);
#4022=ORIENTED_EDGE('',*,*,#2925,.F.);
#4023=ORIENTED_EDGE('',*,*,#2922,.F.);
#4024=ORIENTED_EDGE('',*,*,#2921,.F.);
#4025=ORIENTED_EDGE('',*,*,#2919,.F.);
#4026=ORIENTED_EDGE('',*,*,#2917,.F.);
#4027=ORIENTED_EDGE('',*,*,#3016,.F.);
#4028=ORIENTED_EDGE('',*,*,#3017,.T.);
#4029=ORIENTED_EDGE('',*,*,#3018,.F.);
#4030=ORIENTED_EDGE('',*,*,#2736,.T.);
#4031=ORIENTED_EDGE('',*,*,#2758,.T.);
#4032=ORIENTED_EDGE('',*,*,#2755,.T.);
#4033=ORIENTED_EDGE('',*,*,#2752,.T.);
#4034=ORIENTED_EDGE('',*,*,#2749,.T.);
#4035=ORIENTED_EDGE('',*,*,#2746,.T.);
#4036=ORIENTED_EDGE('',*,*,#2743,.T.);
#4037=ORIENTED_EDGE('',*,*,#2740,.T.);
#4038=ORIENTED_EDGE('',*,*,#2712,.T.);
#4039=ORIENTED_EDGE('',*,*,#2734,.T.);
#4040=ORIENTED_EDGE('',*,*,#2731,.T.);
#4041=ORIENTED_EDGE('',*,*,#2728,.T.);
#4042=ORIENTED_EDGE('',*,*,#2725,.T.);
#4043=ORIENTED_EDGE('',*,*,#2722,.T.);
#4044=ORIENTED_EDGE('',*,*,#2719,.T.);
#4045=ORIENTED_EDGE('',*,*,#2716,.T.);
#4046=ORIENTED_EDGE('',*,*,#2688,.T.);
#4047=ORIENTED_EDGE('',*,*,#2710,.T.);
#4048=ORIENTED_EDGE('',*,*,#2707,.T.);
#4049=ORIENTED_EDGE('',*,*,#2704,.T.);
#4050=ORIENTED_EDGE('',*,*,#2701,.T.);
#4051=ORIENTED_EDGE('',*,*,#2698,.T.);
#4052=ORIENTED_EDGE('',*,*,#2695,.T.);
#4053=ORIENTED_EDGE('',*,*,#2692,.T.);
#4054=ORIENTED_EDGE('',*,*,#2664,.T.);
#4055=ORIENTED_EDGE('',*,*,#2686,.T.);
#4056=ORIENTED_EDGE('',*,*,#2683,.T.);
#4057=ORIENTED_EDGE('',*,*,#2680,.T.);
#4058=ORIENTED_EDGE('',*,*,#2677,.T.);
#4059=ORIENTED_EDGE('',*,*,#2674,.T.);
#4060=ORIENTED_EDGE('',*,*,#2671,.T.);
#4061=ORIENTED_EDGE('',*,*,#2668,.T.);
#4062=ORIENTED_EDGE('',*,*,#2711,.F.);
#4063=ORIENTED_EDGE('',*,*,#2690,.F.);
#4064=ORIENTED_EDGE('',*,*,#2694,.F.);
#4065=ORIENTED_EDGE('',*,*,#2697,.F.);
#4066=ORIENTED_EDGE('',*,*,#2700,.F.);
#4067=ORIENTED_EDGE('',*,*,#2703,.F.);
#4068=ORIENTED_EDGE('',*,*,#2706,.F.);
#4069=ORIENTED_EDGE('',*,*,#2709,.F.);
#4070=ORIENTED_EDGE('',*,*,#3019,.F.);
#4071=ORIENTED_EDGE('',*,*,#2687,.F.);
#4072=ORIENTED_EDGE('',*,*,#2666,.F.);
#4073=ORIENTED_EDGE('',*,*,#2670,.F.);
#4074=ORIENTED_EDGE('',*,*,#2673,.F.);
#4075=ORIENTED_EDGE('',*,*,#2676,.F.);
#4076=ORIENTED_EDGE('',*,*,#2679,.F.);
#4077=ORIENTED_EDGE('',*,*,#2682,.F.);
#4078=ORIENTED_EDGE('',*,*,#2685,.F.);
#4079=ORIENTED_EDGE('',*,*,#2762,.F.);
#4080=ORIENTED_EDGE('',*,*,#2759,.F.);
#4081=ORIENTED_EDGE('',*,*,#2738,.F.);
#4082=ORIENTED_EDGE('',*,*,#2742,.F.);
#4083=ORIENTED_EDGE('',*,*,#2745,.F.);
#4084=ORIENTED_EDGE('',*,*,#2748,.F.);
#4085=ORIENTED_EDGE('',*,*,#2751,.F.);
#4086=ORIENTED_EDGE('',*,*,#2754,.F.);
#4087=ORIENTED_EDGE('',*,*,#2757,.F.);
#4088=ORIENTED_EDGE('',*,*,#2765,.F.);
#4089=ORIENTED_EDGE('',*,*,#2735,.F.);
#4090=ORIENTED_EDGE('',*,*,#2714,.F.);
#4091=ORIENTED_EDGE('',*,*,#2718,.F.);
#4092=ORIENTED_EDGE('',*,*,#2721,.F.);
#4093=ORIENTED_EDGE('',*,*,#2724,.F.);
#4094=ORIENTED_EDGE('',*,*,#2727,.F.);
#4095=ORIENTED_EDGE('',*,*,#2730,.F.);
#4096=ORIENTED_EDGE('',*,*,#2733,.F.);
#4097=ORIENTED_EDGE('',*,*,#3020,.F.);
#4098=ORIENTED_EDGE('',*,*,#3021,.T.);
#4099=ORIENTED_EDGE('',*,*,#3022,.T.);
#4100=ORIENTED_EDGE('',*,*,#2908,.T.);
#4101=ORIENTED_EDGE('',*,*,#3022,.F.);
#4102=ORIENTED_EDGE('',*,*,#3021,.F.);
#4103=ORIENTED_EDGE('',*,*,#3023,.T.);
#4104=ORIENTED_EDGE('',*,*,#3017,.F.);
#4105=ORIENTED_EDGE('',*,*,#3023,.F.);
#4106=ORIENTED_EDGE('',*,*,#3024,.T.);
#4107=ORIENTED_EDGE('',*,*,#3025,.T.);
#4108=ORIENTED_EDGE('',*,*,#2912,.T.);
#4109=ORIENTED_EDGE('',*,*,#3025,.F.);
#4110=ORIENTED_EDGE('',*,*,#3024,.F.);
#4111=ORIENTED_EDGE('',*,*,#3026,.T.);
#4112=ORIENTED_EDGE('',*,*,#3018,.T.);
#4113=ORIENTED_EDGE('',*,*,#3026,.F.);
#4114=ORIENTED_EDGE('',*,*,#2909,.T.);
#4115=ORIENTED_EDGE('',*,*,#3027,.T.);
#4116=ORIENTED_EDGE('',*,*,#3028,.T.);
#4117=ORIENTED_EDGE('',*,*,#3027,.F.);
#4118=ORIENTED_EDGE('',*,*,#3028,.F.);
#4119=ORIENTED_EDGE('',*,*,#3029,.T.);
#4120=ORIENTED_EDGE('',*,*,#3016,.T.);
#4121=ORIENTED_EDGE('',*,*,#3029,.F.);
#4122=ORIENTED_EDGE('',*,*,#2910,.T.);
#4123=ORIENTED_EDGE('',*,*,#3030,.T.);
#4124=ORIENTED_EDGE('',*,*,#3019,.T.);
#4125=ORIENTED_EDGE('',*,*,#3030,.F.);
#4126=ORIENTED_EDGE('',*,*,#2911,.F.);
#4127=ORIENTED_EDGE('',*,*,#3031,.T.);
#4128=ORIENTED_EDGE('',*,*,#3020,.T.);
#4129=ORIENTED_EDGE('',*,*,#3031,.F.);
#4130=ORIENTED_EDGE('',*,*,#2820,.F.);
#4131=ORIENTED_EDGE('',*,*,#2873,.F.);
#4132=ORIENTED_EDGE('',*,*,#2949,.F.);
#4133=ORIENTED_EDGE('',*,*,#3000,.T.);
#4866=PLANE('',#5501);
#4867=PLANE('',#5505);
#4868=PLANE('',#5509);
#4869=PLANE('',#5513);
#4870=PLANE('',#5517);
#4871=PLANE('',#5521);
#4872=PLANE('',#5525);
#4873=PLANE('',#5529);
#4874=PLANE('',#5533);
#4875=PLANE('',#5537);
#4876=PLANE('',#5541);
#4877=PLANE('',#5545);
#4878=PLANE('',#5549);
#4879=PLANE('',#5553);
#4880=PLANE('',#5557);
#4881=PLANE('',#5561);
#4882=PLANE('',#5577);
#4883=PLANE('',#5581);
#4884=PLANE('',#5585);
#4885=PLANE('',#5589);
#4886=PLANE('',#5593);
#4887=PLANE('',#5597);
#4888=PLANE('',#5601);
#4889=PLANE('',#5605);
#4890=PLANE('',#5609);
#4891=PLANE('',#5613);
#4892=PLANE('',#5617);
#4893=PLANE('',#5621);
#4894=PLANE('',#5625);
#4895=PLANE('',#5629);
#4896=PLANE('',#5633);
#4897=PLANE('',#5637);
#4898=PLANE('',#5644);
#4899=PLANE('',#5647);
#4900=PLANE('',#5650);
#4901=PLANE('',#5653);
#4902=PLANE('',#5656);
#4903=PLANE('',#5659);
#4904=PLANE('',#5662);
#4905=PLANE('',#5665);
#4906=PLANE('',#5672);
#4907=PLANE('',#5682);
#4908=PLANE('',#5685);
#4909=PLANE('',#5688);
#4910=PLANE('',#5691);
#4911=PLANE('',#5694);
#4912=PLANE('',#5697);
#4913=PLANE('',#5700);
#4914=PLANE('',#5703);
#4915=PLANE('',#5707);
#4916=PLANE('',#5711);
#4917=PLANE('',#5715);
#4918=PLANE('',#5719);
#4919=PLANE('',#5723);
#4920=PLANE('',#5727);
#4921=PLANE('',#5731);
#4922=PLANE('',#5735);
#4923=PLANE('',#5741);
#4924=PLANE('',#5743);
#4925=PLANE('',#5745);
#4926=PLANE('',#5747);
#4927=PLANE('',#5749);
#4928=PLANE('',#5751);
#4929=PLANE('',#5753);
#4930=PLANE('',#5755);
#4931=PLANE('',#5757);
#4932=PLANE('',#5761);
#4933=PLANE('',#5763);
#4934=PLANE('',#5764);
#4935=PLANE('',#5765);
#5016=ADVANCED_FACE('',(#604),#4866,.F.);
#5017=ADVANCED_FACE('',(#605),#535,.F.);
#5018=ADVANCED_FACE('',(#606),#4867,.F.);
#5019=ADVANCED_FACE('',(#607),#536,.F.);
#5020=ADVANCED_FACE('',(#608),#4868,.F.);
#5021=ADVANCED_FACE('',(#609),#537,.F.);
#5022=ADVANCED_FACE('',(#610),#4869,.F.);
#5023=ADVANCED_FACE('',(#611),#538,.F.);
#5024=ADVANCED_FACE('',(#612),#4870,.F.);
#5025=ADVANCED_FACE('',(#613),#539,.F.);
#5026=ADVANCED_FACE('',(#614),#4871,.F.);
#5027=ADVANCED_FACE('',(#615),#540,.F.);
#5028=ADVANCED_FACE('',(#616),#4872,.F.);
#5029=ADVANCED_FACE('',(#617),#541,.F.);
#5030=ADVANCED_FACE('',(#618),#4873,.F.);
#5031=ADVANCED_FACE('',(#619),#542,.F.);
#5032=ADVANCED_FACE('',(#620),#4874,.F.);
#5033=ADVANCED_FACE('',(#621),#543,.F.);
#5034=ADVANCED_FACE('',(#622),#4875,.F.);
#5035=ADVANCED_FACE('',(#623),#544,.F.);
#5036=ADVANCED_FACE('',(#624),#4876,.F.);
#5037=ADVANCED_FACE('',(#625),#545,.F.);
#5038=ADVANCED_FACE('',(#626),#4877,.F.);
#5039=ADVANCED_FACE('',(#627),#546,.F.);
#5040=ADVANCED_FACE('',(#628),#4878,.F.);
#5041=ADVANCED_FACE('',(#629),#547,.F.);
#5042=ADVANCED_FACE('',(#630),#4879,.F.);
#5043=ADVANCED_FACE('',(#631),#548,.F.);
#5044=ADVANCED_FACE('',(#632),#4880,.F.);
#5045=ADVANCED_FACE('',(#633),#549,.F.);
#5046=ADVANCED_FACE('',(#634),#4881,.F.);
#5047=ADVANCED_FACE('',(#635),#550,.F.);
#5048=ADVANCED_FACE('',(#636),#551,.F.);
#5049=ADVANCED_FACE('',(#637),#552,.F.);
#5050=ADVANCED_FACE('',(#638),#183,.F.);
#5051=ADVANCED_FACE('',(#639),#184,.T.);
#5052=ADVANCED_FACE('',(#640),#4882,.T.);
#5053=ADVANCED_FACE('',(#641),#185,.T.);
#5054=ADVANCED_FACE('',(#642),#4883,.T.);
#5055=ADVANCED_FACE('',(#643),#186,.T.);
#5056=ADVANCED_FACE('',(#644),#4884,.T.);
#5057=ADVANCED_FACE('',(#645),#187,.T.);
#5058=ADVANCED_FACE('',(#646),#4885,.T.);
#5059=ADVANCED_FACE('',(#647),#188,.T.);
#5060=ADVANCED_FACE('',(#648),#4886,.T.);
#5061=ADVANCED_FACE('',(#649),#189,.T.);
#5062=ADVANCED_FACE('',(#650),#4887,.T.);
#5063=ADVANCED_FACE('',(#651),#190,.T.);
#5064=ADVANCED_FACE('',(#652),#4888,.T.);
#5065=ADVANCED_FACE('',(#653),#191,.T.);
#5066=ADVANCED_FACE('',(#654),#4889,.T.);
#5067=ADVANCED_FACE('',(#655),#192,.T.);
#5068=ADVANCED_FACE('',(#656),#4890,.T.);
#5069=ADVANCED_FACE('',(#657),#193,.T.);
#5070=ADVANCED_FACE('',(#658),#4891,.T.);
#5071=ADVANCED_FACE('',(#659),#194,.T.);
#5072=ADVANCED_FACE('',(#660),#4892,.T.);
#5073=ADVANCED_FACE('',(#661),#195,.T.);
#5074=ADVANCED_FACE('',(#662),#4893,.T.);
#5075=ADVANCED_FACE('',(#663),#196,.T.);
#5076=ADVANCED_FACE('',(#664),#4894,.T.);
#5077=ADVANCED_FACE('',(#665),#197,.T.);
#5078=ADVANCED_FACE('',(#666),#4895,.T.);
#5079=ADVANCED_FACE('',(#667),#198,.T.);
#5080=ADVANCED_FACE('',(#668),#4896,.T.);
#5081=ADVANCED_FACE('',(#669),#199,.T.);
#5082=ADVANCED_FACE('',(#670),#4897,.T.);
#5083=ADVANCED_FACE('',(#671),#200,.T.);
#5084=ADVANCED_FACE('',(#672),#201,.F.);
#5085=ADVANCED_FACE('',(#673),#4898,.T.);
#5086=ADVANCED_FACE('',(#674),#553,.T.);
#5087=ADVANCED_FACE('',(#675),#4899,.T.);
#5088=ADVANCED_FACE('',(#676),#554,.T.);
#5089=ADVANCED_FACE('',(#677),#4900,.T.);
#5090=ADVANCED_FACE('',(#678),#555,.T.);
#5091=ADVANCED_FACE('',(#679),#4901,.T.);
#5092=ADVANCED_FACE('',(#680),#556,.T.);
#5093=ADVANCED_FACE('',(#681),#4902,.T.);
#5094=ADVANCED_FACE('',(#682),#557,.T.);
#5095=ADVANCED_FACE('',(#683),#4903,.T.);
#5096=ADVANCED_FACE('',(#684),#558,.T.);
#5097=ADVANCED_FACE('',(#685),#4904,.T.);
#5098=ADVANCED_FACE('',(#686),#559,.T.);
#5099=ADVANCED_FACE('',(#687),#4905,.T.);
#5100=ADVANCED_FACE('',(#688),#560,.T.);
#5101=ADVANCED_FACE('',(#689),#561,.F.);
#5102=ADVANCED_FACE('',(#690),#562,.F.);
#5103=ADVANCED_FACE('',(#691,#132,#133,#134,#135,#136,#137,#138),#4906,
 .T.);
#5104=ADVANCED_FACE('',(#692),#202,.F.);
#5105=ADVANCED_FACE('',(#693),#203,.T.);
#5106=ADVANCED_FACE('',(#694),#4907,.T.);
#5107=ADVANCED_FACE('',(#695),#204,.T.);
#5108=ADVANCED_FACE('',(#696),#4908,.T.);
#5109=ADVANCED_FACE('',(#697),#205,.T.);
#5110=ADVANCED_FACE('',(#698),#4909,.T.);
#5111=ADVANCED_FACE('',(#699),#206,.T.);
#5112=ADVANCED_FACE('',(#700),#4910,.T.);
#5113=ADVANCED_FACE('',(#701),#207,.T.);
#5114=ADVANCED_FACE('',(#702),#4911,.T.);
#5115=ADVANCED_FACE('',(#703),#208,.T.);
#5116=ADVANCED_FACE('',(#704),#4912,.T.);
#5117=ADVANCED_FACE('',(#705),#209,.T.);
#5118=ADVANCED_FACE('',(#706),#4913,.T.);
#5119=ADVANCED_FACE('',(#707),#210,.T.);
#5120=ADVANCED_FACE('',(#708),#4914,.T.);
#5121=ADVANCED_FACE('',(#709),#211,.T.);
#5122=ADVANCED_FACE('',(#710),#4915,.T.);
#5123=ADVANCED_FACE('',(#711),#212,.T.);
#5124=ADVANCED_FACE('',(#712),#4916,.T.);
#5125=ADVANCED_FACE('',(#713),#213,.T.);
#5126=ADVANCED_FACE('',(#714),#4917,.T.);
#5127=ADVANCED_FACE('',(#715),#214,.T.);
#5128=ADVANCED_FACE('',(#716),#4918,.T.);
#5129=ADVANCED_FACE('',(#717),#215,.T.);
#5130=ADVANCED_FACE('',(#718),#4919,.T.);
#5131=ADVANCED_FACE('',(#719),#216,.T.);
#5132=ADVANCED_FACE('',(#720),#4920,.T.);
#5133=ADVANCED_FACE('',(#721),#217,.T.);
#5134=ADVANCED_FACE('',(#722),#4921,.T.);
#5135=ADVANCED_FACE('',(#723),#218,.T.);
#5136=ADVANCED_FACE('',(#724),#4922,.T.);
#5137=ADVANCED_FACE('',(#725),#219,.T.);
#5138=ADVANCED_FACE('',(#726),#220,.F.);
#5139=ADVANCED_FACE('',(#727),#4923,.F.);
#5140=ADVANCED_FACE('',(#728),#563,.T.);
#5141=ADVANCED_FACE('',(#729),#4924,.F.);
#5142=ADVANCED_FACE('',(#730),#564,.T.);
#5143=ADVANCED_FACE('',(#731),#4925,.F.);
#5144=ADVANCED_FACE('',(#732),#565,.T.);
#5145=ADVANCED_FACE('',(#733),#4926,.F.);
#5146=ADVANCED_FACE('',(#734),#566,.T.);
#5147=ADVANCED_FACE('',(#735),#4927,.F.);
#5148=ADVANCED_FACE('',(#736),#567,.T.);
#5149=ADVANCED_FACE('',(#737),#4928,.F.);
#5150=ADVANCED_FACE('',(#738),#568,.T.);
#5151=ADVANCED_FACE('',(#739),#4929,.F.);
#5152=ADVANCED_FACE('',(#740),#569,.T.);
#5153=ADVANCED_FACE('',(#741),#4930,.F.);
#5154=ADVANCED_FACE('',(#742),#570,.T.);
#5155=ADVANCED_FACE('',(#743,#139,#140,#141,#142,#143,#144,#145),#4931,
 .F.);
#5156=ADVANCED_FACE('',(#744,#146),#4932,.T.);
#5157=ADVANCED_FACE('',(#745,#147),#4933,.T.);
#5158=ADVANCED_FACE('',(#746,#148),#4934,.T.);
#5159=ADVANCED_FACE('',(#747,#149),#4935,.T.);
#5160=ADVANCED_FACE('',(#748),#221,.F.);
#5161=ADVANCED_FACE('',(#749),#571,.F.);
#5162=ADVANCED_FACE('',(#750),#222,.F.);
#5163=ADVANCED_FACE('',(#751),#572,.F.);
#5164=ADVANCED_FACE('',(#752),#223,.F.);
#5165=ADVANCED_FACE('',(#753),#573,.F.);
#5166=ADVANCED_FACE('',(#754),#574,.F.);
#5167=ADVANCED_FACE('',(#755),#575,.F.);
#5168=ADVANCED_FACE('',(#756),#576,.T.);
#5342=CLOSED_SHELL('',(#5016,#5017,#5018,#5019,#5020,#5021,#5022,#5023,
#5024,#5025,#5026,#5027,#5028,#5029,#5030,#5031,#5032,#5033,#5034,#5035,
#5036,#5037,#5038,#5039,#5040,#5041,#5042,#5043,#5044,#5045,#5046,#5047,
#5048,#5049,#5050,#5051,#5052,#5053,#5054,#5055,#5056,#5057,#5058,#5059,
#5060,#5061,#5062,#5063,#5064,#5065,#5066,#5067,#5068,#5069,#5070,#5071,
#5072,#5073,#5074,#5075,#5076,#5077,#5078,#5079,#5080,#5081,#5082,#5083,
#5084,#5085,#5086,#5087,#5088,#5089,#5090,#5091,#5092,#5093,#5094,#5095,
#5096,#5097,#5098,#5099,#5100,#5101,#5102,#5103,#5104,#5105,#5106,#5107,
#5108,#5109,#5110,#5111,#5112,#5113,#5114,#5115,#5116,#5117,#5118,#5119,
#5120,#5121,#5122,#5123,#5124,#5125,#5126,#5127,#5128,#5129,#5130,#5131,
#5132,#5133,#5134,#5135,#5136,#5137,#5138,#5139,#5140,#5141,#5142,#5143,
#5144,#5145,#5146,#5147,#5148,#5149,#5150,#5151,#5152,#5153,#5154,#5155,
#5156,#5157,#5158,#5159,#5160,#5161,#5162,#5163,#5164,#5165,#5166,#5167,
#5168));
#5500=AXIS2_PLACEMENT_3D('',#7795,#6112,#6113);
#5501=AXIS2_PLACEMENT_3D('',#7796,#6114,#6115);
#5502=AXIS2_PLACEMENT_3D('',#7805,#6120,#6121);
#5503=AXIS2_PLACEMENT_3D('',#7807,#6122,#6123);
#5504=AXIS2_PLACEMENT_3D('',#7810,#6125,#6126);
#5505=AXIS2_PLACEMENT_3D('',#7811,#6127,#6128);
#5506=AXIS2_PLACEMENT_3D('',#7817,#6132,#6133);
#5507=AXIS2_PLACEMENT_3D('',#7819,#6134,#6135);
#5508=AXIS2_PLACEMENT_3D('',#7822,#6137,#6138);
#5509=AXIS2_PLACEMENT_3D('',#7823,#6139,#6140);
#5510=AXIS2_PLACEMENT_3D('',#7829,#6144,#6145);
#5511=AXIS2_PLACEMENT_3D('',#7831,#6146,#6147);
#5512=AXIS2_PLACEMENT_3D('',#7834,#6149,#6150);
#5513=AXIS2_PLACEMENT_3D('',#7835,#6151,#6152);
#5514=AXIS2_PLACEMENT_3D('',#7841,#6156,#6157);
#5515=AXIS2_PLACEMENT_3D('',#7842,#6158,#6159);
#5516=AXIS2_PLACEMENT_3D('',#7843,#6160,#6161);
#5517=AXIS2_PLACEMENT_3D('',#7844,#6162,#6163);
#5518=AXIS2_PLACEMENT_3D('',#7853,#6168,#6169);
#5519=AXIS2_PLACEMENT_3D('',#7855,#6170,#6171);
#5520=AXIS2_PLACEMENT_3D('',#7858,#6173,#6174);
#5521=AXIS2_PLACEMENT_3D('',#7859,#6175,#6176);
#5522=AXIS2_PLACEMENT_3D('',#7865,#6180,#6181);
#5523=AXIS2_PLACEMENT_3D('',#7867,#6182,#6183);
#5524=AXIS2_PLACEMENT_3D('',#7870,#6185,#6186);
#5525=AXIS2_PLACEMENT_3D('',#7871,#6187,#6188);
#5526=AXIS2_PLACEMENT_3D('',#7877,#6192,#6193);
#5527=AXIS2_PLACEMENT_3D('',#7879,#6194,#6195);
#5528=AXIS2_PLACEMENT_3D('',#7882,#6197,#6198);
#5529=AXIS2_PLACEMENT_3D('',#7883,#6199,#6200);
#5530=AXIS2_PLACEMENT_3D('',#7889,#6204,#6205);
#5531=AXIS2_PLACEMENT_3D('',#7890,#6206,#6207);
#5532=AXIS2_PLACEMENT_3D('',#7891,#6208,#6209);
#5533=AXIS2_PLACEMENT_3D('',#7892,#6210,#6211);
#5534=AXIS2_PLACEMENT_3D('',#7901,#6216,#6217);
#5535=AXIS2_PLACEMENT_3D('',#7903,#6218,#6219);
#5536=AXIS2_PLACEMENT_3D('',#7906,#6221,#6222);
#5537=AXIS2_PLACEMENT_3D('',#7907,#6223,#6224);
#5538=AXIS2_PLACEMENT_3D('',#7913,#6228,#6229);
#5539=AXIS2_PLACEMENT_3D('',#7915,#6230,#6231);
#5540=AXIS2_PLACEMENT_3D('',#7918,#6233,#6234);
#5541=AXIS2_PLACEMENT_3D('',#7919,#6235,#6236);
#5542=AXIS2_PLACEMENT_3D('',#7925,#6240,#6241);
#5543=AXIS2_PLACEMENT_3D('',#7927,#6242,#6243);
#5544=AXIS2_PLACEMENT_3D('',#7930,#6245,#6246);
#5545=AXIS2_PLACEMENT_3D('',#7931,#6247,#6248);
#5546=AXIS2_PLACEMENT_3D('',#7937,#6252,#6253);
#5547=AXIS2_PLACEMENT_3D('',#7938,#6254,#6255);
#5548=AXIS2_PLACEMENT_3D('',#7939,#6256,#6257);
#5549=AXIS2_PLACEMENT_3D('',#7940,#6258,#6259);
#5550=AXIS2_PLACEMENT_3D('',#7949,#6264,#6265);
#5551=AXIS2_PLACEMENT_3D('',#7951,#6266,#6267);
#5552=AXIS2_PLACEMENT_3D('',#7954,#6269,#6270);
#5553=AXIS2_PLACEMENT_3D('',#7955,#6271,#6272);
#5554=AXIS2_PLACEMENT_3D('',#7961,#6276,#6277);
#5555=AXIS2_PLACEMENT_3D('',#7963,#6278,#6279);
#5556=AXIS2_PLACEMENT_3D('',#7966,#6281,#6282);
#5557=AXIS2_PLACEMENT_3D('',#7967,#6283,#6284);
#5558=AXIS2_PLACEMENT_3D('',#7973,#6288,#6289);
#5559=AXIS2_PLACEMENT_3D('',#7975,#6290,#6291);
#5560=AXIS2_PLACEMENT_3D('',#7978,#6293,#6294);
#5561=AXIS2_PLACEMENT_3D('',#7979,#6295,#6296);
#5562=AXIS2_PLACEMENT_3D('',#7985,#6300,#6301);
#5563=AXIS2_PLACEMENT_3D('',#7986,#6302,#6303);
#5564=AXIS2_PLACEMENT_3D('',#7987,#6304,#6305);
#5565=AXIS2_PLACEMENT_3D('',#7988,#6306,#6307);
#5566=AXIS2_PLACEMENT_3D('',#7990,#6308,#6309);
#5567=AXIS2_PLACEMENT_3D('',#7993,#6311,#6312);
#5568=AXIS2_PLACEMENT_3D('',#7994,#6313,#6314);
#5569=AXIS2_PLACEMENT_3D('',#7996,#6315,#6316);
#5570=AXIS2_PLACEMENT_3D('',#7999,#6318,#6319);
#5571=AXIS2_PLACEMENT_3D('',#8000,#6320,#6321);
#5572=AXIS2_PLACEMENT_3D('',#8014,#6322,#6323);
#5573=AXIS2_PLACEMENT_3D('',#8017,#6325,#6326);
#5574=AXIS2_PLACEMENT_3D('',#8018,#6327,#6328);
#5575=AXIS2_PLACEMENT_3D('',#8022,#6330,#6331);
#5576=AXIS2_PLACEMENT_3D('',#8023,#6332,#6333);
#5577=AXIS2_PLACEMENT_3D('',#8024,#6334,#6335);
#5578=AXIS2_PLACEMENT_3D('',#8030,#6339,#6340);
#5579=AXIS2_PLACEMENT_3D('',#8034,#6342,#6343);
#5580=AXIS2_PLACEMENT_3D('',#8035,#6344,#6345);
#5581=AXIS2_PLACEMENT_3D('',#8036,#6346,#6347);
#5582=AXIS2_PLACEMENT_3D('',#8042,#6351,#6352);
#5583=AXIS2_PLACEMENT_3D('',#8046,#6354,#6355);
#5584=AXIS2_PLACEMENT_3D('',#8047,#6356,#6357);
#5585=AXIS2_PLACEMENT_3D('',#8048,#6358,#6359);
#5586=AXIS2_PLACEMENT_3D('',#8054,#6363,#6364);
#5587=AXIS2_PLACEMENT_3D('',#8058,#6366,#6367);
#5588=AXIS2_PLACEMENT_3D('',#8059,#6368,#6369);
#5589=AXIS2_PLACEMENT_3D('',#8060,#6370,#6371);
#5590=AXIS2_PLACEMENT_3D('',#8066,#6375,#6376);
#5591=AXIS2_PLACEMENT_3D('',#8070,#6378,#6379);
#5592=AXIS2_PLACEMENT_3D('',#8071,#6380,#6381);
#5593=AXIS2_PLACEMENT_3D('',#8072,#6382,#6383);
#5594=AXIS2_PLACEMENT_3D('',#8078,#6387,#6388);
#5595=AXIS2_PLACEMENT_3D('',#8082,#6390,#6391);
#5596=AXIS2_PLACEMENT_3D('',#8083,#6392,#6393);
#5597=AXIS2_PLACEMENT_3D('',#8084,#6394,#6395);
#5598=AXIS2_PLACEMENT_3D('',#8090,#6399,#6400);
#5599=AXIS2_PLACEMENT_3D('',#8094,#6402,#6403);
#5600=AXIS2_PLACEMENT_3D('',#8095,#6404,#6405);
#5601=AXIS2_PLACEMENT_3D('',#8096,#6406,#6407);
#5602=AXIS2_PLACEMENT_3D('',#8102,#6411,#6412);
#5603=AXIS2_PLACEMENT_3D('',#8106,#6414,#6415);
#5604=AXIS2_PLACEMENT_3D('',#8107,#6416,#6417);
#5605=AXIS2_PLACEMENT_3D('',#8108,#6418,#6419);
#5606=AXIS2_PLACEMENT_3D('',#8114,#6423,#6424);
#5607=AXIS2_PLACEMENT_3D('',#8116,#6425,#6426);
#5608=AXIS2_PLACEMENT_3D('',#8119,#6428,#6429);
#5609=AXIS2_PLACEMENT_3D('',#8120,#6430,#6431);
#5610=AXIS2_PLACEMENT_3D('',#8126,#6435,#6436);
#5611=AXIS2_PLACEMENT_3D('',#8128,#6437,#6438);
#5612=AXIS2_PLACEMENT_3D('',#8131,#6440,#6441);
#5613=AXIS2_PLACEMENT_3D('',#8132,#6442,#6443);
#5614=AXIS2_PLACEMENT_3D('',#8138,#6447,#6448);
#5615=AXIS2_PLACEMENT_3D('',#8140,#6449,#6450);
#5616=AXIS2_PLACEMENT_3D('',#8143,#6452,#6453);
#5617=AXIS2_PLACEMENT_3D('',#8144,#6454,#6455);
#5618=AXIS2_PLACEMENT_3D('',#8150,#6459,#6460);
#5619=AXIS2_PLACEMENT_3D('',#8152,#6461,#6462);
#5620=AXIS2_PLACEMENT_3D('',#8155,#6464,#6465);
#5621=AXIS2_PLACEMENT_3D('',#8156,#6466,#6467);
#5622=AXIS2_PLACEMENT_3D('',#8162,#6471,#6472);
#5623=AXIS2_PLACEMENT_3D('',#8164,#6473,#6474);
#5624=AXIS2_PLACEMENT_3D('',#8167,#6476,#6477);
#5625=AXIS2_PLACEMENT_3D('',#8168,#6478,#6479);
#5626=AXIS2_PLACEMENT_3D('',#8174,#6483,#6484);
#5627=AXIS2_PLACEMENT_3D('',#8176,#6485,#6486);
#5628=AXIS2_PLACEMENT_3D('',#8179,#6488,#6489);
#5629=AXIS2_PLACEMENT_3D('',#8180,#6490,#6491);
#5630=AXIS2_PLACEMENT_3D('',#8186,#6495,#6496);
#5631=AXIS2_PLACEMENT_3D('',#8188,#6497,#6498);
#5632=AXIS2_PLACEMENT_3D('',#8191,#6500,#6501);
#5633=AXIS2_PLACEMENT_3D('',#8192,#6502,#6503);
#5634=AXIS2_PLACEMENT_3D('',#8198,#6507,#6508);
#5635=AXIS2_PLACEMENT_3D('',#8200,#6509,#6510);
#5636=AXIS2_PLACEMENT_3D('',#8203,#6512,#6513);
#5637=AXIS2_PLACEMENT_3D('',#8204,#6514,#6515);
#5638=AXIS2_PLACEMENT_3D('',#8210,#6519,#6520);
#5639=AXIS2_PLACEMENT_3D('',#8214,#6522,#6523);
#5640=AXIS2_PLACEMENT_3D('',#8215,#6524,#6525);
#5641=AXIS2_PLACEMENT_3D('',#8216,#6526,#6527);
#5642=AXIS2_PLACEMENT_3D('',#8217,#6528,#6529);
#5643=AXIS2_PLACEMENT_3D('',#8218,#6530,#6531);
#5644=AXIS2_PLACEMENT_3D('',#8219,#6532,#6533);
#5645=AXIS2_PLACEMENT_3D('',#8225,#6537,#6538);
#5646=AXIS2_PLACEMENT_3D('',#8228,#6540,#6541);
#5647=AXIS2_PLACEMENT_3D('',#8229,#6542,#6543);
#5648=AXIS2_PLACEMENT_3D('',#8233,#6546,#6547);
#5649=AXIS2_PLACEMENT_3D('',#8236,#6549,#6550);
#5650=AXIS2_PLACEMENT_3D('',#8237,#6551,#6552);
#5651=AXIS2_PLACEMENT_3D('',#8241,#6555,#6556);
#5652=AXIS2_PLACEMENT_3D('',#8244,#6558,#6559);
#5653=AXIS2_PLACEMENT_3D('',#8245,#6560,#6561);
#5654=AXIS2_PLACEMENT_3D('',#8249,#6564,#6565);
#5655=AXIS2_PLACEMENT_3D('',#8252,#6567,#6568);
#5656=AXIS2_PLACEMENT_3D('',#8253,#6569,#6570);
#5657=AXIS2_PLACEMENT_3D('',#8257,#6573,#6574);
#5658=AXIS2_PLACEMENT_3D('',#8260,#6576,#6577);
#5659=AXIS2_PLACEMENT_3D('',#8261,#6578,#6579);
#5660=AXIS2_PLACEMENT_3D('',#8265,#6582,#6583);
#5661=AXIS2_PLACEMENT_3D('',#8268,#6585,#6586);
#5662=AXIS2_PLACEMENT_3D('',#8269,#6587,#6588);
#5663=AXIS2_PLACEMENT_3D('',#8273,#6591,#6592);
#5664=AXIS2_PLACEMENT_3D('',#8276,#6594,#6595);
#5665=AXIS2_PLACEMENT_3D('',#8277,#6596,#6597);
#5666=AXIS2_PLACEMENT_3D('',#8281,#6600,#6601);
#5667=AXIS2_PLACEMENT_3D('',#8284,#6603,#6604);
#5668=AXIS2_PLACEMENT_3D('',#8285,#6605,#6606);
#5669=AXIS2_PLACEMENT_3D('',#8288,#6608,#6609);
#5670=AXIS2_PLACEMENT_3D('',#8289,#6610,#6611);
#5671=AXIS2_PLACEMENT_3D('',#8292,#6613,#6614);
#5672=AXIS2_PLACEMENT_3D('',#8293,#6615,#6616);
#5673=AXIS2_PLACEMENT_3D('',#8295,#6617,#6618);
#5674=AXIS2_PLACEMENT_3D('',#8297,#6619,#6620);
#5675=AXIS2_PLACEMENT_3D('',#8299,#6621,#6622);
#5676=AXIS2_PLACEMENT_3D('',#8301,#6623,#6624);
#5677=AXIS2_PLACEMENT_3D('',#8303,#6625,#6626);
#5678=AXIS2_PLACEMENT_3D('',#8304,#6627,#6628);
#5679=AXIS2_PLACEMENT_3D('',#8317,#6629,#6630);
#5680=AXIS2_PLACEMENT_3D('',#8319,#6632,#6633);
#5681=AXIS2_PLACEMENT_3D('',#8322,#6635,#6636);
#5682=AXIS2_PLACEMENT_3D('',#8323,#6637,#6638);
#5683=AXIS2_PLACEMENT_3D('',#8327,#6641,#6642);
#5684=AXIS2_PLACEMENT_3D('',#8330,#6644,#6645);
#5685=AXIS2_PLACEMENT_3D('',#8331,#6646,#6647);
#5686=AXIS2_PLACEMENT_3D('',#8335,#6650,#6651);
#5687=AXIS2_PLACEMENT_3D('',#8338,#6653,#6654);
#5688=AXIS2_PLACEMENT_3D('',#8339,#6655,#6656);
#5689=AXIS2_PLACEMENT_3D('',#8343,#6659,#6660);
#5690=AXIS2_PLACEMENT_3D('',#8346,#6662,#6663);
#5691=AXIS2_PLACEMENT_3D('',#8347,#6664,#6665);
#5692=AXIS2_PLACEMENT_3D('',#8351,#6668,#6669);
#5693=AXIS2_PLACEMENT_3D('',#8354,#6671,#6672);
#5694=AXIS2_PLACEMENT_3D('',#8355,#6673,#6674);
#5695=AXIS2_PLACEMENT_3D('',#8359,#6677,#6678);
#5696=AXIS2_PLACEMENT_3D('',#8362,#6680,#6681);
#5697=AXIS2_PLACEMENT_3D('',#8363,#6682,#6683);
#5698=AXIS2_PLACEMENT_3D('',#8367,#6686,#6687);
#5699=AXIS2_PLACEMENT_3D('',#8370,#6689,#6690);
#5700=AXIS2_PLACEMENT_3D('',#8371,#6691,#6692);
#5701=AXIS2_PLACEMENT_3D('',#8375,#6695,#6696);
#5702=AXIS2_PLACEMENT_3D('',#8378,#6698,#6699);
#5703=AXIS2_PLACEMENT_3D('',#8379,#6700,#6701);
#5704=AXIS2_PLACEMENT_3D('',#8383,#6704,#6705);
#5705=AXIS2_PLACEMENT_3D('',#8387,#6707,#6708);
#5706=AXIS2_PLACEMENT_3D('',#8388,#6709,#6710);
#5707=AXIS2_PLACEMENT_3D('',#8389,#6711,#6712);
#5708=AXIS2_PLACEMENT_3D('',#8395,#6716,#6717);
#5709=AXIS2_PLACEMENT_3D('',#8397,#6718,#6719);
#5710=AXIS2_PLACEMENT_3D('',#8400,#6721,#6722);
#5711=AXIS2_PLACEMENT_3D('',#8401,#6723,#6724);
#5712=AXIS2_PLACEMENT_3D('',#8407,#6728,#6729);
#5713=AXIS2_PLACEMENT_3D('',#8409,#6730,#6731);
#5714=AXIS2_PLACEMENT_3D('',#8412,#6733,#6734);
#5715=AXIS2_PLACEMENT_3D('',#8413,#6735,#6736);
#5716=AXIS2_PLACEMENT_3D('',#8419,#6740,#6741);
#5717=AXIS2_PLACEMENT_3D('',#8421,#6742,#6743);
#5718=AXIS2_PLACEMENT_3D('',#8424,#6745,#6746);
#5719=AXIS2_PLACEMENT_3D('',#8425,#6747,#6748);
#5720=AXIS2_PLACEMENT_3D('',#8431,#6752,#6753);
#5721=AXIS2_PLACEMENT_3D('',#8433,#6754,#6755);
#5722=AXIS2_PLACEMENT_3D('',#8436,#6757,#6758);
#5723=AXIS2_PLACEMENT_3D('',#8437,#6759,#6760);
#5724=AXIS2_PLACEMENT_3D('',#8443,#6764,#6765);
#5725=AXIS2_PLACEMENT_3D('',#8445,#6766,#6767);
#5726=AXIS2_PLACEMENT_3D('',#8448,#6769,#6770);
#5727=AXIS2_PLACEMENT_3D('',#8449,#6771,#6772);
#5728=AXIS2_PLACEMENT_3D('',#8455,#6776,#6777);
#5729=AXIS2_PLACEMENT_3D('',#8457,#6778,#6779);
#5730=AXIS2_PLACEMENT_3D('',#8460,#6781,#6782);
#5731=AXIS2_PLACEMENT_3D('',#8461,#6783,#6784);
#5732=AXIS2_PLACEMENT_3D('',#8467,#6788,#6789);
#5733=AXIS2_PLACEMENT_3D('',#8469,#6790,#6791);
#5734=AXIS2_PLACEMENT_3D('',#8472,#6793,#6794);
#5735=AXIS2_PLACEMENT_3D('',#8473,#6795,#6796);
#5736=AXIS2_PLACEMENT_3D('',#8479,#6800,#6801);
#5737=AXIS2_PLACEMENT_3D('',#8482,#6803,#6804);
#5738=AXIS2_PLACEMENT_3D('',#8483,#6805,#6806);
#5739=AXIS2_PLACEMENT_3D('',#8484,#6807,#6808);
#5740=AXIS2_PLACEMENT_3D('',#8485,#6809,#6810);
#5741=AXIS2_PLACEMENT_3D('',#8486,#6811,#6812);
#5742=AXIS2_PLACEMENT_3D('',#8489,#6815,#6816);
#5743=AXIS2_PLACEMENT_3D('',#8491,#6818,#6819);
#5744=AXIS2_PLACEMENT_3D('',#8493,#6821,#6822);
#5745=AXIS2_PLACEMENT_3D('',#8495,#6824,#6825);
#5746=AXIS2_PLACEMENT_3D('',#8497,#6827,#6828);
#5747=AXIS2_PLACEMENT_3D('',#8499,#6830,#6831);
#5748=AXIS2_PLACEMENT_3D('',#8501,#6833,#6834);
#5749=AXIS2_PLACEMENT_3D('',#8503,#6836,#6837);
#5750=AXIS2_PLACEMENT_3D('',#8505,#6839,#6840);
#5751=AXIS2_PLACEMENT_3D('',#8507,#6842,#6843);
#5752=AXIS2_PLACEMENT_3D('',#8509,#6845,#6846);
#5753=AXIS2_PLACEMENT_3D('',#8511,#6848,#6849);
#5754=AXIS2_PLACEMENT_3D('',#8513,#6851,#6852);
#5755=AXIS2_PLACEMENT_3D('',#8515,#6854,#6855);
#5756=AXIS2_PLACEMENT_3D('',#8517,#6857,#6858);
#5757=AXIS2_PLACEMENT_3D('',#8518,#6859,#6860);
#5758=AXIS2_PLACEMENT_3D('',#8520,#6861,#6862);
#5759=AXIS2_PLACEMENT_3D('',#8522,#6863,#6864);
#5760=AXIS2_PLACEMENT_3D('',#8524,#6865,#6866);
#5761=AXIS2_PLACEMENT_3D('',#8525,#6867,#6868);
#5762=AXIS2_PLACEMENT_3D('',#8527,#6869,#6870);
#5763=AXIS2_PLACEMENT_3D('',#8528,#6871,#6872);
#5764=AXIS2_PLACEMENT_3D('',#8529,#6873,#6874);
#5765=AXIS2_PLACEMENT_3D('',#8530,#6875,#6876);
#5766=AXIS2_PLACEMENT_3D('',#8532,#6877,#6878);
#5767=AXIS2_PLACEMENT_3D('',#8533,#6879,#6880);
#5768=AXIS2_PLACEMENT_3D('',#8535,#6881,#6882);
#5769=AXIS2_PLACEMENT_3D('',#8537,#6884,#6885);
#5770=AXIS2_PLACEMENT_3D('',#8539,#6887,#6888);
#5771=AXIS2_PLACEMENT_3D('',#8541,#6889,#6890);
#5772=AXIS2_PLACEMENT_3D('',#8543,#6892,#6893);
#5773=AXIS2_PLACEMENT_3D('',#8545,#6895,#6896);
#5774=AXIS2_PLACEMENT_3D('',#8548,#6898,#6899);
#5775=AXIS2_PLACEMENT_3D('',#8549,#6900,#6901);
#5776=AXIS2_PLACEMENT_3D('',#8551,#6903,#6904);
#5777=AXIS2_PLACEMENT_3D('',#8553,#6906,#6907);
#5778=AXIS2_PLACEMENT_3D('',#8555,#6909,#6910);
#6112=DIRECTION('axis',(0.,0.,1.));
#6113=DIRECTION('refdir',(1.,0.,0.));
#6114=DIRECTION('center_axis',(-1.,0.,0.));
#6115=DIRECTION('ref_axis',(0.,1.,3.83915447951421E-33));
#6116=DIRECTION('',(0.,1.,1.22464679914735E-16));
#6117=DIRECTION('',(0.,0.,-1.));
#6118=DIRECTION('',(0.,1.,3.83915447951421E-33));
#6119=DIRECTION('',(0.,0.,-1.));
#6120=DIRECTION('center_axis',(0.,0.,-1.));
#6121=DIRECTION('ref_axis',(-0.717326861318586,0.696736803987579,0.));
#6122=DIRECTION('center_axis',(0.,1.22464679914735E-16,-1.));
#6123=DIRECTION('ref_axis',(-0.717326861318586,0.696736803987579,0.));
#6124=DIRECTION('',(0.,0.,-1.));
#6125=DIRECTION('center_axis',(1.55523680250478E-33,-1.51059548673417E-33,
-1.));
#6126=DIRECTION('ref_axis',(-0.717326861318586,0.696736803987579,-2.16810060569314E-33));
#6127=DIRECTION('center_axis',(-1.,0.,0.));
#6128=DIRECTION('ref_axis',(0.,1.,0.));
#6129=DIRECTION('',(0.,1.,1.22464679914735E-16));
#6130=DIRECTION('',(0.,0.,-1.));
#6131=DIRECTION('',(0.,1.,0.));
#6132=DIRECTION('center_axis',(0.,0.,-1.));
#6133=DIRECTION('ref_axis',(-1.,0.,0.));
#6134=DIRECTION('center_axis',(0.,1.22464679914735E-16,-1.));
#6135=DIRECTION('ref_axis',(-1.,0.,0.));
#6136=DIRECTION('',(0.,0.,-1.));
#6137=DIRECTION('center_axis',(0.,0.,-1.));
#6138=DIRECTION('ref_axis',(-1.,0.,0.));
#6139=DIRECTION('center_axis',(1.,1.87772095759185E-15,0.));
#6140=DIRECTION('ref_axis',(1.87772095759185E-15,-1.,-8.60989605595408E-34));
#6141=DIRECTION('',(1.87772095759185E-15,-1.,-1.22464679914735E-16));
#6142=DIRECTION('',(0.,0.,-1.));
#6143=DIRECTION('',(1.87772095759185E-15,-1.,-8.60989605595408E-34));
#6144=DIRECTION('center_axis',(0.,0.,-1.));
#6145=DIRECTION('ref_axis',(0.747636447008101,-0.664108231469166,0.));
#6146=DIRECTION('center_axis',(0.,1.22464679914735E-16,-1.));
#6147=DIRECTION('ref_axis',(0.747636447008101,-0.664108231469166,0.));
#6148=DIRECTION('',(0.,0.,-1.));
#6149=DIRECTION('center_axis',(3.84526517546801E-34,-3.41566046629928E-34,
-1.));
#6150=DIRECTION('ref_axis',(0.747636447008101,-0.664108231469166,5.14322862516405E-34));
#6151=DIRECTION('center_axis',(1.,9.38860478795921E-16,0.));
#6152=DIRECTION('ref_axis',(9.38860478795921E-16,-1.,2.05736781630139E-32));
#6153=DIRECTION('',(9.38860478795921E-16,-1.,-1.22464679914735E-16));
#6154=DIRECTION('',(0.,0.,-1.));
#6155=DIRECTION('',(9.38860478795921E-16,-1.,2.05736781630139E-32));
#6156=DIRECTION('center_axis',(0.,0.,-1.));
#6157=DIRECTION('ref_axis',(1.,0.,0.));
#6158=DIRECTION('center_axis',(0.,1.22464679914735E-16,-1.));
#6159=DIRECTION('ref_axis',(1.,0.,0.));
#6160=DIRECTION('center_axis',(0.,0.,-1.));
#6161=DIRECTION('ref_axis',(1.,0.,0.));
#6162=DIRECTION('center_axis',(1.98620985225205E-15,-1.,0.));
#6163=DIRECTION('ref_axis',(-1.,-1.98620985225205E-15,0.));
#6164=DIRECTION('',(-1.,-1.98620985225205E-15,-2.43240553799541E-31));
#6165=DIRECTION('',(0.,0.,-1.));
#6166=DIRECTION('',(-1.,-1.98620985225205E-15,0.));
#6167=DIRECTION('',(0.,0.,-1.));
#6168=DIRECTION('center_axis',(0.,0.,-1.));
#6169=DIRECTION('ref_axis',(-0.696736803987579,-0.717326861318586,0.));
#6170=DIRECTION('center_axis',(0.,1.22464679914735E-16,-1.));
#6171=DIRECTION('ref_axis',(-0.696736803987579,-0.717326861318586,0.));
#6172=DIRECTION('',(0.,0.,-1.));
#6173=DIRECTION('center_axis',(6.92366496631146E-48,7.12827402066476E-48,
-1.));
#6174=DIRECTION('ref_axis',(-0.696736803987579,-0.717326861318586,-9.93727463037089E-48));
#6175=DIRECTION('center_axis',(0.,-1.,0.));
#6176=DIRECTION('ref_axis',(-1.,0.,-2.30940147376294E-32));
#6177=DIRECTION('',(-1.,0.,0.));
#6178=DIRECTION('',(0.,0.,-1.));
#6179=DIRECTION('',(-1.,0.,-2.30940147376294E-32));
#6180=DIRECTION('center_axis',(0.,0.,-1.));
#6181=DIRECTION('ref_axis',(-1.33992434006485E-15,-1.,0.));
#6182=DIRECTION('center_axis',(0.,1.22464679914735E-16,-1.));
#6183=DIRECTION('ref_axis',(-1.33992434006485E-15,-1.,0.));
#6184=DIRECTION('',(0.,0.,-1.));
#6185=DIRECTION('center_axis',(0.,0.,-1.));
#6186=DIRECTION('ref_axis',(-1.33992434006485E-15,-1.,0.));
#6187=DIRECTION('center_axis',(7.51088383036733E-15,1.,0.));
#6188=DIRECTION('ref_axis',(1.,-7.51088383036733E-15,-2.05736781630138E-32));
#6189=DIRECTION('',(1.,-7.51088383036733E-15,-9.19817984162697E-31));
#6190=DIRECTION('',(0.,0.,-1.));
#6191=DIRECTION('',(1.,-7.51088383036733E-15,-2.05736781630138E-32));
#6192=DIRECTION('center_axis',(0.,0.,-1.));
#6193=DIRECTION('ref_axis',(0.664108231469163,0.747636447008103,0.));
#6194=DIRECTION('center_axis',(0.,1.22464679914735E-16,-1.));
#6195=DIRECTION('ref_axis',(0.664108231469163,0.747636447008103,0.));
#6196=DIRECTION('',(0.,0.,-1.));
#6197=DIRECTION('center_axis',(8.16185220949039E-33,9.18840920464028E-33,
-1.));
#6198=DIRECTION('ref_axis',(0.664108231469163,0.747636447008103,1.22899428477711E-32));
#6199=DIRECTION('center_axis',(-3.75544191518368E-15,1.,0.));
#6200=DIRECTION('ref_axis',(1.,3.75544191518368E-15,8.60989605595486E-34));
#6201=DIRECTION('',(1.,3.75544191518368E-15,4.5990899208135E-31));
#6202=DIRECTION('',(0.,0.,-1.));
#6203=DIRECTION('',(1.,3.75544191518368E-15,8.60989605595486E-34));
#6204=DIRECTION('center_axis',(0.,0.,-1.));
#6205=DIRECTION('ref_axis',(0.,1.,0.));
#6206=DIRECTION('center_axis',(0.,1.22464679914735E-16,-1.));
#6207=DIRECTION('ref_axis',(0.,1.,0.));
#6208=DIRECTION('center_axis',(0.,0.,-1.));
#6209=DIRECTION('ref_axis',(0.,1.,0.));
#6210=DIRECTION('center_axis',(1.,0.,0.));
#6211=DIRECTION('ref_axis',(0.,-1.,2.50419113937346E-32));
#6212=DIRECTION('',(0.,-1.,-1.22464679914735E-16));
#6213=DIRECTION('',(0.,0.,-1.));
#6214=DIRECTION('',(0.,-1.,2.50419113937346E-32));
#6215=DIRECTION('',(0.,0.,-1.));
#6216=DIRECTION('center_axis',(0.,0.,-1.));
#6217=DIRECTION('ref_axis',(1.,0.,0.));
#6218=DIRECTION('center_axis',(0.,1.22464679914735E-16,-1.));
#6219=DIRECTION('ref_axis',(1.,0.,0.));
#6220=DIRECTION('',(0.,0.,-1.));
#6221=DIRECTION('center_axis',(0.,0.,-1.));
#6222=DIRECTION('ref_axis',(1.,0.,0.));
#6223=DIRECTION('center_axis',(-1.,0.,0.));
#6224=DIRECTION('ref_axis',(0.,1.,-8.04212236896447E-32));
#6225=DIRECTION('',(0.,1.,1.22464679914735E-16));
#6226=DIRECTION('',(0.,0.,-1.));
#6227=DIRECTION('',(0.,1.,-8.04212236896447E-32));
#6228=DIRECTION('center_axis',(0.,0.,-1.));
#6229=DIRECTION('ref_axis',(-0.732481654163345,0.680786770078657,0.));
#6230=DIRECTION('center_axis',(0.,1.22464679914735E-16,-1.));
#6231=DIRECTION('ref_axis',(-0.732481654163345,0.680786770078657,0.));
#6232=DIRECTION('',(0.,0.,-1.));
#6233=DIRECTION('center_axis',(0.,0.,-1.));
#6234=DIRECTION('ref_axis',(-0.732481654163345,0.680786770078657,0.));
#6235=DIRECTION('center_axis',(-1.,0.,0.));
#6236=DIRECTION('ref_axis',(0.,1.,0.));
#6237=DIRECTION('',(0.,1.,1.22464679914735E-16));
#6238=DIRECTION('',(0.,0.,-1.));
#6239=DIRECTION('',(0.,1.,0.));
#6240=DIRECTION('center_axis',(0.,0.,-1.));
#6241=DIRECTION('ref_axis',(-1.,3.0626842058625E-15,0.));
#6242=DIRECTION('center_axis',(0.,1.22464679914735E-16,-1.));
#6243=DIRECTION('ref_axis',(-1.,3.0626842058625E-15,0.));
#6244=DIRECTION('',(0.,0.,-1.));
#6245=DIRECTION('center_axis',(0.,0.,-1.));
#6246=DIRECTION('ref_axis',(-1.,3.0626842058625E-15,0.));
#6247=DIRECTION('center_axis',(1.,0.,0.));
#6248=DIRECTION('ref_axis',(0.,-1.,7.62844485451842E-49));
#6249=DIRECTION('',(0.,-1.,-1.22464679914735E-16));
#6250=DIRECTION('',(0.,0.,-1.));
#6251=DIRECTION('',(0.,-1.,7.62844485451842E-49));
#6252=DIRECTION('center_axis',(0.,0.,-1.));
#6253=DIRECTION('ref_axis',(0.732481654163344,-0.680786770078658,0.));
#6254=DIRECTION('center_axis',(0.,1.22464679914735E-16,-1.));
#6255=DIRECTION('ref_axis',(0.732481654163344,-0.680786770078658,0.));
#6256=DIRECTION('center_axis',(-3.24468512908471E-49,3.01569151445155E-49,
-1.));
#6257=DIRECTION('ref_axis',(0.732481654163344,-0.680786770078658,-4.42971521626826E-49));
#6258=DIRECTION('center_axis',(0.,1.,0.));
#6259=DIRECTION('ref_axis',(1.,0.,0.));
#6260=DIRECTION('',(1.,0.,0.));
#6261=DIRECTION('',(0.,0.,-1.));
#6262=DIRECTION('',(1.,0.,0.));
#6263=DIRECTION('',(0.,0.,-1.));
#6264=DIRECTION('center_axis',(0.,0.,-1.));
#6265=DIRECTION('ref_axis',(0.680786770078658,0.732481654163344,0.));
#6266=DIRECTION('center_axis',(0.,1.22464679914735E-16,-1.));
#6267=DIRECTION('ref_axis',(0.680786770078658,0.732481654163344,0.));
#6268=DIRECTION('',(0.,0.,-1.));
#6269=DIRECTION('center_axis',(0.,0.,-1.));
#6270=DIRECTION('ref_axis',(0.680786770078658,0.732481654163344,0.));
#6271=DIRECTION('center_axis',(0.,1.,0.));
#6272=DIRECTION('ref_axis',(1.,0.,0.));
#6273=DIRECTION('',(1.,0.,0.));
#6274=DIRECTION('',(0.,0.,-1.));
#6275=DIRECTION('',(1.,0.,0.));
#6276=DIRECTION('center_axis',(0.,0.,-1.));
#6277=DIRECTION('ref_axis',(0.,1.,0.));
#6278=DIRECTION('center_axis',(0.,1.22464679914735E-16,-1.));
#6279=DIRECTION('ref_axis',(0.,1.,0.));
#6280=DIRECTION('',(0.,0.,-1.));
#6281=DIRECTION('center_axis',(0.,0.,-1.));
#6282=DIRECTION('ref_axis',(0.,1.,0.));
#6283=DIRECTION('center_axis',(0.,-1.,0.));
#6284=DIRECTION('ref_axis',(-1.,0.,-6.35647172290725E-34));
#6285=DIRECTION('',(-1.,0.,0.));
#6286=DIRECTION('',(0.,0.,-1.));
#6287=DIRECTION('',(-1.,0.,-6.35647172290725E-34));
#6288=DIRECTION('center_axis',(0.,0.,-1.));
#6289=DIRECTION('ref_axis',(-0.680786770078657,-0.732481654163345,0.));
#6290=DIRECTION('center_axis',(0.,1.22464679914735E-16,-1.));
#6291=DIRECTION('ref_axis',(-0.680786770078657,-0.732481654163345,0.));
#6292=DIRECTION('',(0.,0.,-1.));
#6293=DIRECTION('center_axis',(-2.51285264587953E-34,-2.70366367799702E-34,
-1.));
#6294=DIRECTION('ref_axis',(-0.680786770078657,-0.732481654163345,3.69110087963254E-34));
#6295=DIRECTION('center_axis',(0.,-1.,0.));
#6296=DIRECTION('ref_axis',(-1.,0.,0.));
#6297=DIRECTION('',(-1.,0.,0.));
#6298=DIRECTION('',(0.,0.,-1.));
#6299=DIRECTION('',(-1.,0.,0.));
#6300=DIRECTION('center_axis',(0.,0.,-1.));
#6301=DIRECTION('ref_axis',(-1.91417762866406E-16,-1.,0.));
#6302=DIRECTION('center_axis',(0.,1.22464679914735E-16,-1.));
#6303=DIRECTION('ref_axis',(-1.91417762866406E-16,-1.,0.));
#6304=DIRECTION('center_axis',(0.,0.,-1.));
#6305=DIRECTION('ref_axis',(-1.91417762866406E-16,-1.,0.));
#6306=DIRECTION('center_axis',(0.,1.22464679914735E-16,-1.));
#6307=DIRECTION('ref_axis',(1.,0.,0.));
#6308=DIRECTION('center_axis',(0.,-1.22464679914735E-16,1.));
#6309=DIRECTION('ref_axis',(1.,0.,0.));
#6310=DIRECTION('',(0.,-1.22464679914735E-16,1.));
#6311=DIRECTION('center_axis',(-3.84526517546801E-34,3.41566046629928E-34,
1.));
#6312=DIRECTION('ref_axis',(1.,0.,0.));
#6313=DIRECTION('center_axis',(0.,-1.22464679914735E-16,1.));
#6314=DIRECTION('ref_axis',(-2.22044604925031E-16,1.,1.22464679914735E-16));
#6315=DIRECTION('center_axis',(0.,1.22464679914735E-16,-1.));
#6316=DIRECTION('ref_axis',(-2.22044604925031E-16,1.,1.22464679914735E-16));
#6317=DIRECTION('',(0.,-1.22464679914735E-16,1.));
#6318=DIRECTION('center_axis',(0.,0.,1.));
#6319=DIRECTION('ref_axis',(-2.22044604925031E-16,1.,1.22464679914735E-16));
#6320=DIRECTION('center_axis',(0.,1.22464679914735E-16,-1.));
#6321=DIRECTION('ref_axis',(-2.22044604925031E-16,1.,1.22464679914735E-16));
#6322=DIRECTION('center_axis',(0.,1.22464679914735E-16,-1.));
#6323=DIRECTION('ref_axis',(-2.22044604925031E-16,1.,1.22464679914735E-16));
#6324=DIRECTION('',(-0.707098477694133,0.00342678313306322,0.707106781186547));
#6325=DIRECTION('center_axis',(0.,-1.22464679914735E-16,1.));
#6326=DIRECTION('ref_axis',(-2.22044604925031E-16,1.,1.22464679914735E-16));
#6327=DIRECTION('center_axis',(0.,-1.22464679914735E-16,1.));
#6328=DIRECTION('ref_axis',(-0.999997064267793,0.00242310870464513,2.96745231912974E-19));
#6329=DIRECTION('',(-0.707106781186563,-8.65956056235474E-17,0.707106781186532));
#6330=DIRECTION('center_axis',(0.,1.22464679914735E-16,-1.));
#6331=DIRECTION('ref_axis',(-0.999997064267793,0.00242310870464512,2.96745231912974E-19));
#6332=DIRECTION('center_axis',(0.,-1.22464679914735E-16,1.));
#6333=DIRECTION('ref_axis',(-0.999997064267794,0.00242310870464513,2.96745231912974E-19));
#6334=DIRECTION('center_axis',(-0.707106781186548,-7.04136402448282E-17,
-0.707106781186548));
#6335=DIRECTION('ref_axis',(0.707106781186548,8.65956056235493E-17,-0.707106781186548));
#6336=DIRECTION('',(-0.707106781186547,-8.65956056235493E-17,0.707106781186547));
#6337=DIRECTION('',(-2.22044604925031E-16,1.,1.22464679914735E-16));
#6338=DIRECTION('',(2.22044604925031E-16,-1.,-1.22464679914735E-16));
#6339=DIRECTION('center_axis',(0.,-1.22464679914735E-16,1.));
#6340=DIRECTION('ref_axis',(-1.,-1.20644235342523E-14,-1.47746576647801E-30));
#6341=DIRECTION('',(-0.70568734200296,-0.0447814173156507,0.707106781186547));
#6342=DIRECTION('center_axis',(0.,1.22464679914735E-16,-1.));
#6343=DIRECTION('ref_axis',(-1.,-1.20644235342523E-14,-1.47746576647801E-30));
#6344=DIRECTION('center_axis',(0.,-1.22464679914735E-16,1.));
#6345=DIRECTION('ref_axis',(-1.,-1.20644235342523E-14,-1.47746576647801E-30));
#6346=DIRECTION('center_axis',(-0.705687342002958,-0.0447814173156751,-0.707106781186548));
#6347=DIRECTION('ref_axis',(0.707816856590716,8.65085590544045E-17,-0.706395992008758));
#6348=DIRECTION('',(-0.705687342002958,-0.0447814173156759,0.707106781186547));
#6349=DIRECTION('',(-0.0633304877101172,0.997992609855604,1.22218845523238E-16));
#6350=DIRECTION('',(0.0633304877101172,-0.997992609855604,-1.22218845523238E-16));
#6351=DIRECTION('center_axis',(0.,-1.22464679914735E-16,1.));
#6352=DIRECTION('ref_axis',(-0.997992609855603,-0.0633304877101176,-7.75574790626363E-18));
#6353=DIRECTION('',(-0.495178732794061,-0.504775219863721,0.707106781186547));
#6354=DIRECTION('center_axis',(0.,1.22464679914735E-16,-1.));
#6355=DIRECTION('ref_axis',(-0.997992609855603,-0.0633304877101176,-7.75574790626363E-18));
#6356=DIRECTION('center_axis',(0.,-1.22464679914735E-16,1.));
#6357=DIRECTION('ref_axis',(-0.997992609855603,-0.0633304877101176,-7.75574790626363E-18));
#6358=DIRECTION('center_axis',(-0.495178732794066,-0.504775219863718,-0.707106781186546));
#6359=DIRECTION('ref_axis',(0.819120891857568,7.02483028577243E-17,-0.573620924062627));
#6360=DIRECTION('',(-0.495178732794064,-0.504775219863716,0.707106781186549));
#6361=DIRECTION('',(-0.71385996188113,0.700288479716089,8.57606045164075E-17));
#6362=DIRECTION('',(0.71385996188113,-0.700288479716089,-8.57606045164075E-17));
#6363=DIRECTION('center_axis',(0.,-1.22464679914735E-16,1.));
#6364=DIRECTION('ref_axis',(-0.700288479716085,-0.713859961881135,-8.74226317357183E-17));
#6365=DIRECTION('',(-4.71027737605131E-15,-0.707106781186549,0.707106781186546));
#6366=DIRECTION('center_axis',(0.,1.22464679914735E-16,-1.));
#6367=DIRECTION('ref_axis',(-0.700288479716085,-0.713859961881135,-8.74226317357183E-17));
#6368=DIRECTION('center_axis',(0.,-1.22464679914735E-16,1.));
#6369=DIRECTION('ref_axis',(-0.700288479716085,-0.713859961881135,-8.74226317357183E-17));
#6370=DIRECTION('center_axis',(1.57009245868378E-16,-0.707106781186549,
-0.707106781186546));
#6371=DIRECTION('ref_axis',(1.,-2.71926214689379E-32,2.22044604925032E-16));
#6372=DIRECTION('',(0.,-0.707106781186546,0.707106781186549));
#6373=DIRECTION('',(-1.,-2.22044604925031E-16,-2.71926214689378E-32));
#6374=DIRECTION('',(1.,2.22044604925031E-16,2.71926214689378E-32));
#6375=DIRECTION('center_axis',(0.,-1.22464679914735E-16,1.));
#6376=DIRECTION('ref_axis',(-1.44328993201271E-15,-1.,-1.22464679914735E-16));
#6377=DIRECTION('',(0.501258447848715,-0.498738376767117,0.707106781186546));
#6378=DIRECTION('center_axis',(0.,1.22464679914735E-16,-1.));
#6379=DIRECTION('ref_axis',(-1.44328993201271E-15,-1.,-1.22464679914735E-16));
#6380=DIRECTION('center_axis',(0.,-1.22464679914735E-16,1.));
#6381=DIRECTION('ref_axis',(-1.44328993201271E-15,-1.,-1.22464679914735E-16));
#6382=DIRECTION('center_axis',(0.501258447848716,-0.498738376767119,-0.707106781186545));
#6383=DIRECTION('ref_axis',(0.815811569646784,-7.08235047989531E-17,0.578317804351942));
#6384=DIRECTION('',(0.501258447848714,-0.498738376767113,0.70710678118655));
#6385=DIRECTION('',(-0.705322576499999,-0.708886495201738,-8.68135577307594E-17));
#6386=DIRECTION('',(0.705322576499999,0.708886495201738,8.68135577307594E-17));
#6387=DIRECTION('center_axis',(0.,-1.22464679914735E-16,1.));
#6388=DIRECTION('ref_axis',(0.708886495201743,-0.705322576499993,-8.63771035677081E-17));
#6389=DIRECTION('',(0.702660115090392,-0.0791755180668618,0.707106781186548));
#6390=DIRECTION('center_axis',(0.,1.22464679914735E-16,-1.));
#6391=DIRECTION('ref_axis',(0.708886495201743,-0.705322576499994,-8.63771035677081E-17));
#6392=DIRECTION('center_axis',(0.,-1.22464679914735E-16,1.));
#6393=DIRECTION('ref_axis',(0.708886495201743,-0.705322576499994,-8.63771035677081E-17));
#6394=DIRECTION('center_axis',(0.702660115090393,-0.0791755180668588,-0.707106781186547));
#6395=DIRECTION('ref_axis',(0.709333598508651,-8.63220376296547E-17,0.704872928992714));
#6396=DIRECTION('',(0.702660115090393,-0.0791755180668555,0.707106781186548));
#6397=DIRECTION('',(-0.111971091458068,-0.993711464499474,-1.21694556427531E-16));
#6398=DIRECTION('',(0.111971091458068,0.993711464499474,1.21694556427531E-16));
#6399=DIRECTION('center_axis',(0.,-1.22464679914735E-16,1.));
#6400=DIRECTION('ref_axis',(0.993711464499475,-0.111971091458059,-1.37125038751148E-17));
#6401=DIRECTION('',(0.707106781186547,-1.26473352750937E-14,0.707106781186548));
#6402=DIRECTION('center_axis',(0.,1.22464679914735E-16,-1.));
#6403=DIRECTION('ref_axis',(0.993711464499475,-0.111971091458059,-1.37125038751148E-17));
#6404=DIRECTION('center_axis',(0.,-1.22464679914735E-16,1.));
#6405=DIRECTION('ref_axis',(0.993711464499475,-0.111971091458059,-1.37125038751148E-17));
#6406=DIRECTION('center_axis',(0.707106781186548,2.43045314947538E-16,-0.707106781186547));
#6407=DIRECTION('ref_axis',(0.707106781186547,-8.65956056235494E-17,0.707106781186548));
#6408=DIRECTION('',(0.707106781186547,-8.65956056235494E-17,0.707106781186548));
#6409=DIRECTION('',(2.21253300755314E-16,-1.,-1.22464679914735E-16));
#6410=DIRECTION('',(-2.21253300755314E-16,1.,1.22464679914735E-16));
#6411=DIRECTION('center_axis',(0.,-1.22464679914735E-16,1.));
#6412=DIRECTION('ref_axis',(1.,3.92278802034127E-15,4.80402979284452E-31));
#6413=DIRECTION('',(0.701854257103615,0.0860267504066733,0.707106781186548));
#6414=DIRECTION('center_axis',(0.,1.22464679914735E-16,-1.));
#6415=DIRECTION('ref_axis',(1.,3.92278802034127E-15,4.80402979284452E-31));
#6416=DIRECTION('center_axis',(0.,-1.22464679914735E-16,1.));
#6417=DIRECTION('ref_axis',(1.,3.92278802034127E-15,4.80402979284452E-31));
#6418=DIRECTION('center_axis',(0.701854257103617,0.0860267504066795,-0.707106781186545));
#6419=DIRECTION('ref_axis',(0.709737901988185,-8.62721828028444E-17,0.704465833437938));
#6420=DIRECTION('',(0.701854257103612,0.0860267504066774,0.70710678118655));
#6421=DIRECTION('',(0.121660197152011,-0.992571809205225,-1.21554988906708E-16));
#6422=DIRECTION('',(-0.121660197152011,0.992571809205225,1.21554988906708E-16));
#6423=DIRECTION('center_axis',(0.,-1.22464679914735E-16,1.));
#6424=DIRECTION('ref_axis',(0.12166019715201,0.992571809205225,1.21554988906708E-16));
#6425=DIRECTION('center_axis',(0.,-1.22464679914735E-16,1.));
#6426=DIRECTION('ref_axis',(0.12166019715201,0.992571809205225,1.21554988906708E-16));
#6427=DIRECTION('',(0.0860267504066787,0.701854257103615,0.707106781186548));
#6428=DIRECTION('center_axis',(0.,1.22464679914735E-16,-1.));
#6429=DIRECTION('ref_axis',(0.12166019715201,0.992571809205225,1.21554988906708E-16));
#6430=DIRECTION('center_axis',(0.0860267504066789,0.701854257103615,-0.707106781186548));
#6431=DIRECTION('ref_axis',(0.992680551218392,-1.4790024070839E-17,0.120769711570196));
#6432=DIRECTION('',(-0.992571809205225,0.121660197152011,1.48990771025846E-17));
#6433=DIRECTION('',(0.086026750406678,0.701854257103615,0.707106781186548));
#6434=DIRECTION('',(0.992571809205225,-0.121660197152011,-1.48990771025846E-17));
#6435=DIRECTION('center_axis',(0.,-1.22464679914735E-16,1.));
#6436=DIRECTION('ref_axis',(3.70074341541624E-15,1.,1.22464679914735E-16));
#6437=DIRECTION('center_axis',(0.,-1.22464679914735E-16,1.));
#6438=DIRECTION('ref_axis',(3.70074341541624E-15,1.,1.22464679914735E-16));
#6439=DIRECTION('',(3.14018491736755E-15,0.707106781186547,0.707106781186548));
#6440=DIRECTION('center_axis',(0.,1.22464679914735E-16,-1.));
#6441=DIRECTION('ref_axis',(3.70074341541624E-15,1.,1.22464679914735E-16));
#6442=DIRECTION('center_axis',(-5.59536544388552E-19,0.707106781186548,
-0.707106781186547));
#6443=DIRECTION('ref_axis',(1.,9.69068118596694E-35,-7.91304169717666E-19));
#6444=DIRECTION('',(-1.,-7.91304169717665E-19,-9.69068118596693E-35));
#6445=DIRECTION('',(0.,0.707106781186547,0.707106781186548));
#6446=DIRECTION('',(1.,7.91304169717665E-19,9.69068118596693E-35));
#6447=DIRECTION('center_axis',(0.,-1.22464679914735E-16,1.));
#6448=DIRECTION('ref_axis',(-0.111971091458059,0.993711464499475,1.21694556427531E-16));
#6449=DIRECTION('center_axis',(0.,-1.22464679914735E-16,1.));
#6450=DIRECTION('ref_axis',(-0.111971091458059,0.993711464499475,1.21694556427531E-16));
#6451=DIRECTION('',(-0.0791755180668554,0.702660115090393,0.707106781186548));
#6452=DIRECTION('center_axis',(0.,1.22464679914735E-16,-1.));
#6453=DIRECTION('ref_axis',(-0.111971091458059,0.993711464499475,1.21694556427531E-16));
#6454=DIRECTION('center_axis',(-0.0791755180668589,0.702660115090393,-0.707106781186548));
#6455=DIRECTION('ref_axis',(0.993789574232718,1.36273433877159E-17,-0.111275703306486));
#6456=DIRECTION('',(-0.993711464499474,-0.111971091458068,-1.37125038751159E-17));
#6457=DIRECTION('',(-0.0791755180668615,0.702660115090393,0.707106781186547));
#6458=DIRECTION('',(0.993711464499474,0.111971091458068,1.37125038751159E-17));
#6459=DIRECTION('center_axis',(0.,-1.22464679914735E-16,1.));
#6460=DIRECTION('ref_axis',(-0.705322576499994,0.708886495201743,8.681355773076E-17));
#6461=DIRECTION('center_axis',(0.,-1.22464679914735E-16,1.));
#6462=DIRECTION('ref_axis',(-0.705322576499994,0.708886495201743,8.681355773076E-17));
#6463=DIRECTION('',(-0.498738376767112,0.501258447848717,0.707106781186548));
#6464=DIRECTION('center_axis',(0.,1.22464679914735E-16,-1.));
#6465=DIRECTION('ref_axis',(-0.705322576499994,0.708886495201743,8.681355773076E-17));
#6466=DIRECTION('center_axis',(-0.498738376767117,0.501258447848714,-0.707106781186547));
#6467=DIRECTION('ref_axis',(0.817183320658714,7.05859283223419E-17,-0.576377845199829));
#6468=DIRECTION('',(-0.708886495201738,-0.705322576499999,-8.63771035677088E-17));
#6469=DIRECTION('',(-0.498738376767117,0.501258447848713,0.707106781186547));
#6470=DIRECTION('',(0.708886495201738,0.705322576499999,8.63771035677088E-17));
#6471=DIRECTION('center_axis',(0.,-1.22464679914735E-16,1.));
#6472=DIRECTION('ref_axis',(-1.,-1.66533453693774E-15,-2.03944661017034E-31));
#6473=DIRECTION('center_axis',(0.,-1.22464679914735E-16,1.));
#6474=DIRECTION('ref_axis',(-1.,-1.66533453693774E-15,-2.03944661017034E-31));
#6475=DIRECTION('',(-0.707106781186549,-1.65668806430732E-15,0.707106781186546));
#6476=DIRECTION('center_axis',(0.,1.22464679914735E-16,-1.));
#6477=DIRECTION('ref_axis',(-1.,-1.66533453693774E-15,-2.03944661017034E-31));
#6478=DIRECTION('center_axis',(-0.707106781186549,8.65956056235491E-17,
-0.707106781186546));
#6479=DIRECTION('ref_axis',(0.707106781186546,8.65956056235495E-17,-0.707106781186549));
#6480=DIRECTION('',(0.,-1.,-1.22464679914735E-16));
#6481=DIRECTION('',(-0.707106781186546,-8.65956056235495E-17,0.707106781186549));
#6482=DIRECTION('',(0.,1.,1.22464679914735E-16));
#6483=DIRECTION('center_axis',(0.,-1.22464679914735E-16,1.));
#6484=DIRECTION('ref_axis',(-0.713859961881135,-0.700288479716084,-8.57606045164069E-17));
#6485=DIRECTION('center_axis',(0.,-1.22464679914735E-16,1.));
#6486=DIRECTION('ref_axis',(-0.713859961881135,-0.700288479716085,-8.57606045164069E-17));
#6487=DIRECTION('',(-0.504775219863721,-0.495178732794061,0.707106781186547));
#6488=DIRECTION('center_axis',(0.,1.22464679914735E-16,-1.));
#6489=DIRECTION('ref_axis',(-0.713859961881135,-0.700288479716085,-8.57606045164069E-17));
#6490=DIRECTION('center_axis',(-0.504775219863718,-0.495178732794066,-0.707106781186546));
#6491=DIRECTION('ref_axis',(0.813897332858798,7.11530468011979E-17,-0.581008719009737));
#6492=DIRECTION('',(0.700288479716089,-0.71385996188113,-8.74226317357177E-17));
#6493=DIRECTION('',(-0.504775219863716,-0.495178732794063,0.70710678118655));
#6494=DIRECTION('',(-0.700288479716089,0.71385996188113,8.74226317357177E-17));
#6495=DIRECTION('center_axis',(0.,-1.22464679914735E-16,1.));
#6496=DIRECTION('ref_axis',(-0.0633304877101173,-0.997992609855603,-1.22218845523238E-16));
#6497=DIRECTION('center_axis',(0.,-1.22464679914735E-16,1.));
#6498=DIRECTION('ref_axis',(-0.0633304877101173,-0.997992609855603,-1.22218845523238E-16));
#6499=DIRECTION('',(-0.0447814173156758,-0.705687342002959,0.707106781186547));
#6500=DIRECTION('center_axis',(0.,1.22464679914735E-16,-1.));
#6501=DIRECTION('ref_axis',(-0.0633304877101173,-0.997992609855604,-1.22218845523238E-16));
#6502=DIRECTION('center_axis',(-0.044781417315675,-0.705687342002958,-0.707106781186548));
#6503=DIRECTION('ref_axis',(0.998000636867369,7.74024134983379E-18,-0.0632038670678178));
#6504=DIRECTION('',(0.997992609855604,-0.063330487710117,-7.75574790626356E-18));
#6505=DIRECTION('',(-0.0447814173156758,-0.705687342002958,0.707106781186547));
#6506=DIRECTION('',(-0.997992609855604,0.063330487710117,7.75574790626356E-18));
#6507=DIRECTION('center_axis',(0.,-1.22464679914735E-16,1.));
#6508=DIRECTION('ref_axis',(-1.18423789293273E-14,-1.,-1.22464679914735E-16));
#6509=DIRECTION('center_axis',(0.,-1.22464679914735E-16,1.));
#6510=DIRECTION('ref_axis',(-1.18423789293273E-14,-1.,-1.22464679914735E-16));
#6511=DIRECTION('',(-6.28036983473509E-15,-0.707106781186548,0.707106781186547));
#6512=DIRECTION('center_axis',(0.,1.22464679914735E-16,-1.));
#6513=DIRECTION('ref_axis',(-1.18423789293273E-14,-1.,-1.22464679914735E-16));
#6514=DIRECTION('center_axis',(0.,-0.707106781186547,-0.707106781186548));
#6515=DIRECTION('ref_axis',(1.,0.,0.));
#6516=DIRECTION('',(1.,0.,0.));
#6517=DIRECTION('',(0.,-0.707106781186554,0.707106781186541));
#6518=DIRECTION('',(-1.,0.,0.));
#6519=DIRECTION('center_axis',(0.,-1.22464679914735E-16,1.));
#6520=DIRECTION('ref_axis',(0.00242310870467221,-0.999997064267793,-1.2246432039123E-16));
#6521=DIRECTION('',(0.0034267831331041,-0.707098477694138,0.707106781186541));
#6522=DIRECTION('center_axis',(0.,1.22464679914735E-16,-1.));
#6523=DIRECTION('ref_axis',(0.00242310870467221,-0.999997064267793,-1.2246432039123E-16));
#6524=DIRECTION('center_axis',(0.,-1.22464679914735E-16,1.));
#6525=DIRECTION('ref_axis',(0.00242310870467221,-0.999997064267793,-1.2246432039123E-16));
#6526=DIRECTION('center_axis',(0.,1.22464679914735E-16,-1.));
#6527=DIRECTION('ref_axis',(1.,0.,0.));
#6528=DIRECTION('center_axis',(0.,-1.22464679914735E-16,1.));
#6529=DIRECTION('ref_axis',(1.,0.,0.));
#6530=DIRECTION('center_axis',(0.,1.22464679914735E-16,-1.));
#6531=DIRECTION('ref_axis',(1.,0.,0.));
#6532=DIRECTION('center_axis',(0.121660197152011,0.992571809205225,1.21554988906708E-16));
#6533=DIRECTION('ref_axis',(0.992571809205225,-0.121660197152011,-1.48990771025846E-17));
#6534=DIRECTION('',(0.,1.22464679914735E-16,-1.));
#6535=DIRECTION('',(-0.992571809205225,0.121660197152011,1.48990771025846E-17));
#6536=DIRECTION('',(0.,1.22464679914735E-16,-1.));
#6537=DIRECTION('center_axis',(0.,1.22464679914735E-16,-1.));
#6538=DIRECTION('ref_axis',(3.70074341541624E-15,1.,1.22464679914735E-16));
#6539=DIRECTION('',(0.,1.22464679914735E-16,-1.));
#6540=DIRECTION('center_axis',(0.,-1.22464679914735E-16,1.));
#6541=DIRECTION('ref_axis',(3.70074341541624E-15,1.,1.22464679914735E-16));
#6542=DIRECTION('center_axis',(-7.91304169717665E-19,1.,1.22464679914735E-16));
#6543=DIRECTION('ref_axis',(1.,7.91304169717665E-19,9.69068118596693E-35));
#6544=DIRECTION('',(0.,1.22464679914735E-16,-1.));
#6545=DIRECTION('',(-1.,-7.91304169717665E-19,-9.69068118596693E-35));
#6546=DIRECTION('center_axis',(0.,1.22464679914735E-16,-1.));
#6547=DIRECTION('ref_axis',(-0.111971091458059,0.993711464499475,1.21694556427531E-16));
#6548=DIRECTION('',(0.,1.22464679914735E-16,-1.));
#6549=DIRECTION('center_axis',(0.,-1.22464679914735E-16,1.));
#6550=DIRECTION('ref_axis',(-0.111971091458059,0.993711464499475,1.21694556427531E-16));
#6551=DIRECTION('center_axis',(-0.111971091458068,0.993711464499474,1.21694556427531E-16));
#6552=DIRECTION('ref_axis',(0.993711464499474,0.111971091458068,1.37125038751159E-17));
#6553=DIRECTION('',(0.,1.22464679914735E-16,-1.));
#6554=DIRECTION('',(-0.993711464499474,-0.111971091458068,-1.37125038751159E-17));
#6555=DIRECTION('center_axis',(0.,1.22464679914735E-16,-1.));
#6556=DIRECTION('ref_axis',(-0.705322576499994,0.708886495201743,8.681355773076E-17));
#6557=DIRECTION('',(0.,1.22464679914735E-16,-1.));
#6558=DIRECTION('center_axis',(0.,-1.22464679914735E-16,1.));
#6559=DIRECTION('ref_axis',(-0.705322576499994,0.708886495201743,8.681355773076E-17));
#6560=DIRECTION('center_axis',(-0.705322576499999,0.708886495201738,8.68135577307594E-17));
#6561=DIRECTION('ref_axis',(0.708886495201738,0.705322576499999,8.63771035677088E-17));
#6562=DIRECTION('',(0.,1.22464679914735E-16,-1.));
#6563=DIRECTION('',(-0.708886495201738,-0.705322576499999,-8.63771035677088E-17));
#6564=DIRECTION('center_axis',(0.,1.22464679914735E-16,-1.));
#6565=DIRECTION('ref_axis',(-1.,-1.66533453693774E-15,-2.03944661017034E-31));
#6566=DIRECTION('',(0.,1.22464679914735E-16,-1.));
#6567=DIRECTION('center_axis',(0.,-1.22464679914735E-16,1.));
#6568=DIRECTION('ref_axis',(-1.,-1.66533453693774E-15,-2.03944661017034E-31));
#6569=DIRECTION('center_axis',(-1.,0.,0.));
#6570=DIRECTION('ref_axis',(0.,1.,1.22464679914735E-16));
#6571=DIRECTION('',(0.,1.22464679914735E-16,-1.));
#6572=DIRECTION('',(0.,-1.,-1.22464679914735E-16));
#6573=DIRECTION('center_axis',(0.,1.22464679914735E-16,-1.));
#6574=DIRECTION('ref_axis',(-0.713859961881135,-0.700288479716085,-8.57606045164069E-17));
#6575=DIRECTION('',(0.,1.22464679914735E-16,-1.));
#6576=DIRECTION('center_axis',(0.,-1.22464679914735E-16,1.));
#6577=DIRECTION('ref_axis',(-0.713859961881135,-0.700288479716085,-8.57606045164069E-17));
#6578=DIRECTION('center_axis',(-0.71385996188113,-0.700288479716089,-8.57606045164075E-17));
#6579=DIRECTION('ref_axis',(-0.700288479716089,0.71385996188113,8.74226317357177E-17));
#6580=DIRECTION('',(0.,1.22464679914735E-16,-1.));
#6581=DIRECTION('',(0.700288479716089,-0.71385996188113,-8.74226317357177E-17));
#6582=DIRECTION('center_axis',(0.,1.22464679914735E-16,-1.));
#6583=DIRECTION('ref_axis',(-0.0633304877101173,-0.997992609855604,-1.22218845523238E-16));
#6584=DIRECTION('',(0.,1.22464679914735E-16,-1.));
#6585=DIRECTION('center_axis',(0.,-1.22464679914735E-16,1.));
#6586=DIRECTION('ref_axis',(-0.0633304877101173,-0.997992609855604,-1.22218845523238E-16));
#6587=DIRECTION('center_axis',(-0.063330487710117,-0.997992609855603,-1.22218845523238E-16));
#6588=DIRECTION('ref_axis',(-0.997992609855604,0.063330487710117,7.75574790626356E-18));
#6589=DIRECTION('',(0.,1.22464679914735E-16,-1.));
#6590=DIRECTION('',(0.997992609855604,-0.063330487710117,-7.75574790626356E-18));
#6591=DIRECTION('center_axis',(0.,1.22464679914735E-16,-1.));
#6592=DIRECTION('ref_axis',(-1.18423789293273E-14,-1.,-1.22464679914735E-16));
#6593=DIRECTION('',(0.,1.22464679914735E-16,-1.));
#6594=DIRECTION('center_axis',(0.,-1.22464679914735E-16,1.));
#6595=DIRECTION('ref_axis',(-1.18423789293273E-14,-1.,-1.22464679914735E-16));
#6596=DIRECTION('center_axis',(0.,-1.,-1.22464679914735E-16));
#6597=DIRECTION('ref_axis',(-1.,0.,0.));
#6598=DIRECTION('',(0.,1.22464679914735E-16,-1.));
#6599=DIRECTION('',(1.,0.,0.));
#6600=DIRECTION('center_axis',(0.,1.22464679914735E-16,-1.));
#6601=DIRECTION('ref_axis',(0.00242310870467221,-0.999997064267793,-1.2246432039123E-16));
#6602=DIRECTION('',(0.,-1.22464679914735E-16,1.));
#6603=DIRECTION('center_axis',(0.,-1.22464679914735E-16,1.));
#6604=DIRECTION('ref_axis',(0.00242310870467221,-0.999997064267793,-1.2246432039123E-16));
#6605=DIRECTION('center_axis',(0.,1.22464679914735E-16,-1.));
#6606=DIRECTION('ref_axis',(1.,0.,0.));
#6607=DIRECTION('',(0.,1.22464679914735E-16,-1.));
#6608=DIRECTION('center_axis',(0.,1.22464679914735E-16,-1.));
#6609=DIRECTION('ref_axis',(1.,0.,0.));
#6610=DIRECTION('center_axis',(0.,-1.22464679914735E-16,1.));
#6611=DIRECTION('ref_axis',(-2.22044604925031E-16,1.,1.22464679914735E-16));
#6612=DIRECTION('',(0.,1.22464679914735E-16,-1.));
#6613=DIRECTION('center_axis',(0.,1.22464679914735E-16,-1.));
#6614=DIRECTION('ref_axis',(-2.22044604925031E-16,1.,1.22464679914735E-16));
#6615=DIRECTION('center_axis',(0.,1.22464679914735E-16,-1.));
#6616=DIRECTION('ref_axis',(1.,0.,0.));
#6617=DIRECTION('center_axis',(0.,1.22464679914735E-16,-1.));
#6618=DIRECTION('ref_axis',(-2.22044604925031E-16,1.,1.22464679914735E-16));
#6619=DIRECTION('center_axis',(0.,1.22464679914735E-16,-1.));
#6620=DIRECTION('ref_axis',(1.,0.,0.));
#6621=DIRECTION('center_axis',(0.,1.22464679914735E-16,-1.));
#6622=DIRECTION('ref_axis',(-2.22044604925031E-16,1.,1.22464679914735E-16));
#6623=DIRECTION('center_axis',(0.,-1.22464679914735E-16,1.));
#6624=DIRECTION('ref_axis',(1.,0.,0.));
#6625=DIRECTION('center_axis',(0.,1.22464679914735E-16,-1.));
#6626=DIRECTION('ref_axis',(1.,0.,0.));
#6627=DIRECTION('center_axis',(0.,-1.22464679914735E-16,1.));
#6628=DIRECTION('ref_axis',(1.,0.,0.));
#6629=DIRECTION('center_axis',(0.,-1.22464679914735E-16,1.));
#6630=DIRECTION('ref_axis',(1.,0.,0.));
#6631=DIRECTION('',(0.00342678313310414,-0.707098477694131,-0.707106781186548));
#6632=DIRECTION('center_axis',(0.,1.22464679914735E-16,-1.));
#6633=DIRECTION('ref_axis',(0.00242310870467221,-0.999997064267793,-1.2246432039123E-16));
#6634=DIRECTION('',(0.,-0.707106781186554,-0.707106781186541));
#6635=DIRECTION('center_axis',(0.,1.22464679914735E-16,-1.));
#6636=DIRECTION('ref_axis',(0.00242310870467221,-0.999997064267793,-1.2246432039123E-16));
#6637=DIRECTION('center_axis',(0.,-0.707106781186547,0.707106781186548));
#6638=DIRECTION('ref_axis',(-1.,0.,0.));
#6639=DIRECTION('',(0.,-0.707106781186548,-0.707106781186547));
#6640=DIRECTION('',(-1.,0.,0.));
#6641=DIRECTION('center_axis',(0.,1.22464679914735E-16,-1.));
#6642=DIRECTION('ref_axis',(-1.18423789293273E-14,-1.,-1.22464679914735E-16));
#6643=DIRECTION('',(-0.0447814173156507,-0.70568734200296,-0.707106781186546));
#6644=DIRECTION('center_axis',(0.,1.22464679914735E-16,-1.));
#6645=DIRECTION('ref_axis',(-1.18423789293273E-14,-1.,-1.22464679914735E-16));
#6646=DIRECTION('center_axis',(-0.044781417315675,-0.705687342002957,0.707106781186548));
#6647=DIRECTION('ref_axis',(-0.998000636867369,7.74024134983378E-18,-0.0632038670678177));
#6648=DIRECTION('',(-0.997992609855604,0.063330487710117,7.75574790626356E-18));
#6649=DIRECTION('',(-0.0447814173156758,-0.705687342002958,-0.707106781186547));
#6650=DIRECTION('center_axis',(0.,1.22464679914735E-16,-1.));
#6651=DIRECTION('ref_axis',(-0.0633304877101173,-0.997992609855603,-1.22218845523238E-16));
#6652=DIRECTION('',(-0.504775219863726,-0.495178732794059,-0.707106781186545));
#6653=DIRECTION('center_axis',(0.,1.22464679914735E-16,-1.));
#6654=DIRECTION('ref_axis',(-0.0633304877101173,-0.997992609855603,-1.22218845523238E-16));
#6655=DIRECTION('center_axis',(-0.504775219863718,-0.495178732794066,0.707106781186546));
#6656=DIRECTION('ref_axis',(-0.813897332858798,7.11530468011978E-17,-0.581008719009737));
#6657=DIRECTION('',(-0.700288479716089,0.71385996188113,8.74226317357177E-17));
#6658=DIRECTION('',(-0.504775219863717,-0.495178732794063,-0.707106781186549));
#6659=DIRECTION('center_axis',(0.,1.22464679914735E-16,-1.));
#6660=DIRECTION('ref_axis',(-0.713859961881135,-0.700288479716084,-8.57606045164069E-17));
#6661=DIRECTION('',(-0.707106781186546,-4.62368177042778E-15,-0.707106781186549));
#6662=DIRECTION('center_axis',(0.,1.22464679914735E-16,-1.));
#6663=DIRECTION('ref_axis',(-0.713859961881135,-0.700288479716085,-8.57606045164069E-17));
#6664=DIRECTION('center_axis',(-0.707106781186549,-8.65956056235492E-17,
0.707106781186546));
#6665=DIRECTION('ref_axis',(-0.707106781186546,8.65956056235495E-17,-0.707106781186549));
#6666=DIRECTION('',(0.,1.,1.22464679914735E-16));
#6667=DIRECTION('',(-0.707106781186546,8.65956056235495E-17,-0.707106781186549));
#6668=DIRECTION('center_axis',(0.,1.22464679914735E-16,-1.));
#6669=DIRECTION('ref_axis',(-1.,-1.66533453693774E-15,-2.03944661017034E-31));
#6670=DIRECTION('',(-0.498738376767117,0.501258447848715,-0.707106781186546));
#6671=DIRECTION('center_axis',(0.,1.22464679914735E-16,-1.));
#6672=DIRECTION('ref_axis',(-1.,-1.66533453693774E-15,-2.03944661017034E-31));
#6673=DIRECTION('center_axis',(-0.498738376767116,0.501258447848713,0.707106781186548));
#6674=DIRECTION('ref_axis',(-0.817183320658714,7.05859283223419E-17,-0.576377845199828));
#6675=DIRECTION('',(0.708886495201738,0.705322576499999,8.63771035677088E-17));
#6676=DIRECTION('',(-0.498738376767118,0.501258447848713,-0.707106781186547));
#6677=DIRECTION('center_axis',(0.,1.22464679914735E-16,-1.));
#6678=DIRECTION('ref_axis',(-0.705322576499994,0.708886495201743,8.681355773076E-17));
#6679=DIRECTION('',(-0.0791755180668617,0.702660115090393,-0.707106781186547));
#6680=DIRECTION('center_axis',(0.,1.22464679914735E-16,-1.));
#6681=DIRECTION('ref_axis',(-0.705322576499994,0.708886495201743,8.681355773076E-17));
#6682=DIRECTION('center_axis',(-0.0791755180668589,0.702660115090392,0.707106781186549));
#6683=DIRECTION('ref_axis',(-0.993789574232718,1.36273433877158E-17,-0.111275703306486));
#6684=DIRECTION('',(0.993711464499474,0.111971091458068,1.37125038751159E-17));
#6685=DIRECTION('',(-0.0791755180668616,0.702660115090394,-0.707106781186547));
#6686=DIRECTION('center_axis',(0.,1.22464679914735E-16,-1.));
#6687=DIRECTION('ref_axis',(-0.111971091458059,0.993711464499475,1.21694556427531E-16));
#6688=DIRECTION('',(-1.25607396694702E-14,0.707106781186547,-0.707106781186548));
#6689=DIRECTION('center_axis',(0.,1.22464679914735E-16,-1.));
#6690=DIRECTION('ref_axis',(-0.111971091458059,0.993711464499475,1.21694556427531E-16));
#6691=DIRECTION('center_axis',(-5.59536544388551E-19,0.707106781186547,
0.707106781186548));
#6692=DIRECTION('ref_axis',(-1.,9.69068118596692E-35,-7.91304169717664E-19));
#6693=DIRECTION('',(0.,0.707106781186548,-0.707106781186547));
#6694=DIRECTION('',(1.,7.91304169717665E-19,9.69068118596693E-35));
#6695=DIRECTION('center_axis',(0.,1.22464679914735E-16,-1.));
#6696=DIRECTION('ref_axis',(3.70074341541624E-15,1.,1.22464679914735E-16));
#6697=DIRECTION('',(0.086026750406675,0.701854257103615,-0.707106781186548));
#6698=DIRECTION('center_axis',(0.,1.22464679914735E-16,-1.));
#6699=DIRECTION('ref_axis',(3.70074341541624E-15,1.,1.22464679914735E-16));
#6700=DIRECTION('center_axis',(0.086026750406679,0.701854257103615,0.707106781186547));
#6701=DIRECTION('ref_axis',(-0.992680551218392,-1.4790024070839E-17,0.120769711570196));
#6702=DIRECTION('',(0.0860267504066797,0.701854257103614,-0.707106781186548));
#6703=DIRECTION('',(0.992571809205225,-0.121660197152011,-1.48990771025846E-17));
#6704=DIRECTION('center_axis',(0.,1.22464679914735E-16,-1.));
#6705=DIRECTION('ref_axis',(0.12166019715201,0.992571809205225,1.21554988906708E-16));
#6706=DIRECTION('',(0.701854257103614,0.0860267504066782,-0.707106781186548));
#6707=DIRECTION('center_axis',(0.,-1.22464679914735E-16,1.));
#6708=DIRECTION('ref_axis',(0.12166019715201,0.992571809205225,1.21554988906708E-16));
#6709=DIRECTION('center_axis',(0.,1.22464679914735E-16,-1.));
#6710=DIRECTION('ref_axis',(0.12166019715201,0.992571809205225,1.21554988906708E-16));
#6711=DIRECTION('center_axis',(0.701854257103616,0.0860267504066792,0.707106781186546));
#6712=DIRECTION('ref_axis',(-0.709737901988186,-8.62721828028442E-17,0.704465833437937));
#6713=DIRECTION('',(0.121660197152011,-0.992571809205225,-1.21554988906708E-16));
#6714=DIRECTION('',(0.701854257103613,0.0860267504066799,-0.707106781186549));
#6715=DIRECTION('',(-0.121660197152011,0.992571809205225,1.21554988906708E-16));
#6716=DIRECTION('center_axis',(0.,1.22464679914735E-16,-1.));
#6717=DIRECTION('ref_axis',(1.,3.92278802034127E-15,4.80402979284452E-31));
#6718=DIRECTION('center_axis',(0.,1.22464679914735E-16,-1.));
#6719=DIRECTION('ref_axis',(1.,3.92278802034127E-15,4.80402979284452E-31));
#6720=DIRECTION('',(0.707106781186547,1.65668806430733E-15,-0.707106781186548));
#6721=DIRECTION('center_axis',(0.,-1.22464679914735E-16,1.));
#6722=DIRECTION('ref_axis',(1.,3.92278802034127E-15,4.80402979284452E-31));
#6723=DIRECTION('center_axis',(0.707106781186548,6.98541037004396E-17,0.707106781186547));
#6724=DIRECTION('ref_axis',(-0.707106781186547,-8.65956056235493E-17,0.707106781186548));
#6725=DIRECTION('',(2.21253300755314E-16,-1.,-1.22464679914735E-16));
#6726=DIRECTION('',(0.707106781186547,8.65956056235493E-17,-0.707106781186548));
#6727=DIRECTION('',(-2.21253300755314E-16,1.,1.22464679914735E-16));
#6728=DIRECTION('center_axis',(0.,1.22464679914735E-16,-1.));
#6729=DIRECTION('ref_axis',(0.993711464499475,-0.111971091458059,-1.37125038751148E-17));
#6730=DIRECTION('center_axis',(0.,1.22464679914735E-16,-1.));
#6731=DIRECTION('ref_axis',(0.993711464499475,-0.111971091458059,-1.37125038751148E-17));
#6732=DIRECTION('',(0.702660115090394,-0.0791755180668553,-0.707106781186547));
#6733=DIRECTION('center_axis',(0.,-1.22464679914735E-16,1.));
#6734=DIRECTION('ref_axis',(0.993711464499475,-0.111971091458059,-1.37125038751148E-17));
#6735=DIRECTION('center_axis',(0.702660115090393,-0.0791755180668589,0.707106781186548));
#6736=DIRECTION('ref_axis',(-0.709333598508652,-8.63220376296546E-17,0.704872928992714));
#6737=DIRECTION('',(0.702660115090394,-0.0791755180668553,-0.707106781186547));
#6738=DIRECTION('',(0.111971091458068,0.993711464499474,1.21694556427531E-16));
#6739=DIRECTION('',(-0.111971091458068,-0.993711464499474,-1.21694556427531E-16));
#6740=DIRECTION('center_axis',(0.,1.22464679914735E-16,-1.));
#6741=DIRECTION('ref_axis',(0.708886495201743,-0.705322576499993,-8.63771035677081E-17));
#6742=DIRECTION('center_axis',(0.,1.22464679914735E-16,-1.));
#6743=DIRECTION('ref_axis',(0.708886495201743,-0.705322576499994,-8.63771035677081E-17));
#6744=DIRECTION('',(0.501258447848718,-0.498738376767112,-0.707106781186548));
#6745=DIRECTION('center_axis',(0.,-1.22464679914735E-16,1.));
#6746=DIRECTION('ref_axis',(0.708886495201743,-0.705322576499994,-8.63771035677081E-17));
#6747=DIRECTION('center_axis',(0.501258447848716,-0.498738376767119,0.707106781186545));
#6748=DIRECTION('ref_axis',(-0.815811569646784,-7.08235047989531E-17,0.578317804351942));
#6749=DIRECTION('',(0.501258447848714,-0.498738376767113,-0.70710678118655));
#6750=DIRECTION('',(0.705322576499999,0.708886495201738,8.68135577307594E-17));
#6751=DIRECTION('',(-0.705322576499999,-0.708886495201738,-8.68135577307594E-17));
#6752=DIRECTION('center_axis',(0.,1.22464679914735E-16,-1.));
#6753=DIRECTION('ref_axis',(-1.44328993201271E-15,-1.,-1.22464679914735E-16));
#6754=DIRECTION('center_axis',(0.,1.22464679914735E-16,-1.));
#6755=DIRECTION('ref_axis',(-1.44328993201271E-15,-1.,-1.22464679914735E-16));
#6756=DIRECTION('',(-7.85046229341885E-16,-0.707106781186549,-0.707106781186546));
#6757=DIRECTION('center_axis',(0.,-1.22464679914735E-16,1.));
#6758=DIRECTION('ref_axis',(-1.44328993201271E-15,-1.,-1.22464679914735E-16));
#6759=DIRECTION('center_axis',(1.57009245868378E-16,-0.707106781186549,
0.707106781186546));
#6760=DIRECTION('ref_axis',(-1.,-2.71926214689379E-32,2.22044604925032E-16));
#6761=DIRECTION('',(0.,-0.707106781186546,-0.707106781186549));
#6762=DIRECTION('',(1.,2.22044604925031E-16,2.71926214689378E-32));
#6763=DIRECTION('',(-1.,-2.22044604925031E-16,-2.71926214689378E-32));
#6764=DIRECTION('center_axis',(0.,1.22464679914735E-16,-1.));
#6765=DIRECTION('ref_axis',(-0.700288479716085,-0.713859961881135,-8.74226317357183E-17));
#6766=DIRECTION('center_axis',(0.,1.22464679914735E-16,-1.));
#6767=DIRECTION('ref_axis',(-0.700288479716085,-0.713859961881135,-8.74226317357183E-17));
#6768=DIRECTION('',(-0.495178732794061,-0.504775219863721,-0.707106781186547));
#6769=DIRECTION('center_axis',(0.,-1.22464679914735E-16,1.));
#6770=DIRECTION('ref_axis',(-0.700288479716085,-0.713859961881135,-8.74226317357183E-17));
#6771=DIRECTION('center_axis',(-0.495178732794066,-0.504775219863719,0.707106781186546));
#6772=DIRECTION('ref_axis',(-0.819120891857569,7.02483028577242E-17,-0.573620924062626));
#6773=DIRECTION('',(-0.495178732794064,-0.504775219863716,-0.707106781186549));
#6774=DIRECTION('',(0.71385996188113,-0.700288479716089,-8.57606045164075E-17));
#6775=DIRECTION('',(-0.71385996188113,0.700288479716089,8.57606045164075E-17));
#6776=DIRECTION('center_axis',(0.,1.22464679914735E-16,-1.));
#6777=DIRECTION('ref_axis',(-0.997992609855603,-0.0633304877101176,-7.75574790626363E-18));
#6778=DIRECTION('center_axis',(0.,1.22464679914735E-16,-1.));
#6779=DIRECTION('ref_axis',(-0.997992609855603,-0.0633304877101176,-7.75574790626363E-18));
#6780=DIRECTION('',(-0.705687342002959,-0.0447814173156757,-0.707106781186546));
#6781=DIRECTION('center_axis',(0.,-1.22464679914735E-16,1.));
#6782=DIRECTION('ref_axis',(-0.997992609855603,-0.0633304877101176,-7.75574790626363E-18));
#6783=DIRECTION('center_axis',(-0.705687342002957,-0.0447814173156752,0.707106781186548));
#6784=DIRECTION('ref_axis',(-0.707816856590717,8.65085590544045E-17,-0.706395992008758));
#6785=DIRECTION('',(-0.705687342002958,-0.0447814173156758,-0.707106781186547));
#6786=DIRECTION('',(0.0633304877101172,-0.997992609855604,-1.22218845523238E-16));
#6787=DIRECTION('',(-0.0633304877101172,0.997992609855604,1.22218845523238E-16));
#6788=DIRECTION('center_axis',(0.,1.22464679914735E-16,-1.));
#6789=DIRECTION('ref_axis',(-1.,-1.20644235342523E-14,-1.47746576647801E-30));
#6790=DIRECTION('center_axis',(0.,1.22464679914735E-16,-1.));
#6791=DIRECTION('ref_axis',(-1.,-1.20644235342523E-14,-1.47746576647801E-30));
#6792=DIRECTION('',(-0.707106781186549,-6.19377422911154E-15,-0.707106781186546));
#6793=DIRECTION('center_axis',(0.,-1.22464679914735E-16,1.));
#6794=DIRECTION('ref_axis',(-1.,-1.20644235342523E-14,-1.47746576647801E-30));
#6795=DIRECTION('center_axis',(-0.707106781186547,-2.43604851491927E-16,
0.707106781186548));
#6796=DIRECTION('ref_axis',(-0.707106781186548,8.65956056235493E-17,-0.707106781186547));
#6797=DIRECTION('',(-2.22044604925031E-16,1.,1.22464679914735E-16));
#6798=DIRECTION('',(-0.707106781186544,8.65956056235498E-17,-0.707106781186551));
#6799=DIRECTION('',(2.22044604925031E-16,-1.,-1.22464679914735E-16));
#6800=DIRECTION('center_axis',(0.,1.22464679914735E-16,-1.));
#6801=DIRECTION('ref_axis',(-0.999997064267793,0.00242310870464513,2.96745231912974E-19));
#6802=DIRECTION('',(-0.707098477694137,0.00342678313306651,-0.707106781186542));
#6803=DIRECTION('center_axis',(0.,-1.22464679914735E-16,1.));
#6804=DIRECTION('ref_axis',(-0.999997064267793,0.00242310870464512,2.96745231912974E-19));
#6805=DIRECTION('center_axis',(0.,1.22464679914735E-16,-1.));
#6806=DIRECTION('ref_axis',(-0.999997064267794,0.00242310870464513,2.96745231912974E-19));
#6807=DIRECTION('center_axis',(0.,-1.22464679914735E-16,1.));
#6808=DIRECTION('ref_axis',(-2.22044604925031E-16,1.,1.22464679914735E-16));
#6809=DIRECTION('center_axis',(0.,-1.22464679914735E-16,1.));
#6810=DIRECTION('ref_axis',(-2.22044604925031E-16,1.,1.22464679914735E-16));
#6811=DIRECTION('center_axis',(-0.992571809205225,-0.121660197152011,-1.48990771025846E-17));
#6812=DIRECTION('ref_axis',(-0.121660197152011,0.992571809205225,1.21554988906708E-16));
#6813=DIRECTION('',(0.,1.22464679914735E-16,-1.));
#6814=DIRECTION('',(0.,1.22464679914735E-16,-1.));
#6815=DIRECTION('center_axis',(0.,-1.22464679914735E-16,1.));
#6816=DIRECTION('ref_axis',(1.,3.92278802034127E-15,4.80402979284452E-31));
#6817=DIRECTION('',(0.,1.22464679914735E-16,-1.));
#6818=DIRECTION('center_axis',(-1.,-2.21253300755314E-16,-2.70957146570782E-32));
#6819=DIRECTION('ref_axis',(-2.21253300755314E-16,1.,1.22464679914735E-16));
#6820=DIRECTION('',(0.,1.22464679914735E-16,-1.));
#6821=DIRECTION('center_axis',(0.,-1.22464679914735E-16,1.));
#6822=DIRECTION('ref_axis',(0.993711464499475,-0.111971091458059,-1.37125038751148E-17));
#6823=DIRECTION('',(0.,1.22464679914735E-16,-1.));
#6824=DIRECTION('center_axis',(-0.993711464499474,0.111971091458068,1.37125038751158E-17));
#6825=DIRECTION('ref_axis',(0.111971091458068,0.993711464499474,1.21694556427531E-16));
#6826=DIRECTION('',(0.,1.22464679914735E-16,-1.));
#6827=DIRECTION('center_axis',(0.,-1.22464679914735E-16,1.));
#6828=DIRECTION('ref_axis',(0.708886495201743,-0.705322576499994,-8.63771035677081E-17));
#6829=DIRECTION('',(0.,1.22464679914735E-16,-1.));
#6830=DIRECTION('center_axis',(-0.708886495201738,0.705322576499999,8.63771035677088E-17));
#6831=DIRECTION('ref_axis',(0.705322576499999,0.708886495201738,8.68135577307594E-17));
#6832=DIRECTION('',(0.,1.22464679914735E-16,-1.));
#6833=DIRECTION('center_axis',(0.,-1.22464679914735E-16,1.));
#6834=DIRECTION('ref_axis',(-1.44328993201271E-15,-1.,-1.22464679914735E-16));
#6835=DIRECTION('',(0.,1.22464679914735E-16,-1.));
#6836=DIRECTION('center_axis',(-2.22044604925031E-16,1.,1.22464679914735E-16));
#6837=DIRECTION('ref_axis',(1.,2.22044604925031E-16,2.71926214689378E-32));
#6838=DIRECTION('',(0.,1.22464679914735E-16,-1.));
#6839=DIRECTION('center_axis',(0.,-1.22464679914735E-16,1.));
#6840=DIRECTION('ref_axis',(-0.700288479716085,-0.713859961881135,-8.74226317357183E-17));
#6841=DIRECTION('',(0.,1.22464679914735E-16,-1.));
#6842=DIRECTION('center_axis',(0.700288479716089,0.71385996188113,8.74226317357178E-17));
#6843=DIRECTION('ref_axis',(0.71385996188113,-0.700288479716089,-8.57606045164075E-17));
#6844=DIRECTION('',(0.,1.22464679914735E-16,-1.));
#6845=DIRECTION('center_axis',(0.,-1.22464679914735E-16,1.));
#6846=DIRECTION('ref_axis',(-0.997992609855604,-0.0633304877101176,-7.75574790626363E-18));
#6847=DIRECTION('',(0.,1.22464679914735E-16,-1.));
#6848=DIRECTION('center_axis',(0.997992609855603,0.0633304877101172,7.75574790626358E-18));
#6849=DIRECTION('ref_axis',(0.0633304877101172,-0.997992609855604,-1.22218845523238E-16));
#6850=DIRECTION('',(0.,1.22464679914735E-16,-1.));
#6851=DIRECTION('center_axis',(0.,-1.22464679914735E-16,1.));
#6852=DIRECTION('ref_axis',(-1.,-1.20644235342523E-14,-1.47746576647801E-30));
#6853=DIRECTION('',(0.,1.22464679914735E-16,-1.));
#6854=DIRECTION('center_axis',(1.,2.22044604925031E-16,2.71926214689378E-32));
#6855=DIRECTION('ref_axis',(2.22044604925031E-16,-1.,-1.22464679914735E-16));
#6856=DIRECTION('',(0.,-1.22464679914735E-16,1.));
#6857=DIRECTION('center_axis',(0.,1.22464679914735E-16,-1.));
#6858=DIRECTION('ref_axis',(-0.999997064267793,0.00242310870464513,2.96745231912974E-19));
#6859=DIRECTION('center_axis',(0.,1.22464679914735E-16,-1.));
#6860=DIRECTION('ref_axis',(1.,0.,0.));
#6861=DIRECTION('center_axis',(0.,-1.22464679914735E-16,1.));
#6862=DIRECTION('ref_axis',(1.,0.,0.));
#6863=DIRECTION('center_axis',(0.,1.22464679914735E-16,-1.));
#6864=DIRECTION('ref_axis',(-2.22044604925031E-16,1.,1.22464679914735E-16));
#6865=DIRECTION('center_axis',(0.,-1.22464679914735E-16,1.));
#6866=DIRECTION('ref_axis',(-2.22044604925031E-16,1.,1.22464679914735E-16));
#6867=DIRECTION('center_axis',(0.,-1.22464679914735E-16,1.));
#6868=DIRECTION('ref_axis',(1.,0.,0.));
#6869=DIRECTION('center_axis',(-8.16185220949039E-33,-9.18840920464028E-33,
1.));
#6870=DIRECTION('ref_axis',(-2.22044604925031E-16,1.,1.22464679914735E-16));
#6871=DIRECTION('center_axis',(0.,-1.22464679914735E-16,1.));
#6872=DIRECTION('ref_axis',(1.,0.,0.));
#6873=DIRECTION('center_axis',(0.,-1.22464679914735E-16,1.));
#6874=DIRECTION('ref_axis',(1.,0.,0.));
#6875=DIRECTION('center_axis',(0.,-1.22464679914735E-16,1.));
#6876=DIRECTION('ref_axis',(1.,0.,0.));
#6877=DIRECTION('center_axis',(3.24468512908471E-49,-3.01569151445155E-49,
1.));
#6878=DIRECTION('ref_axis',(1.,0.,0.));
#6879=DIRECTION('center_axis',(0.,1.22464679914735E-16,-1.));
#6880=DIRECTION('ref_axis',(-2.22044604925031E-16,1.,1.22464679914735E-16));
#6881=DIRECTION('center_axis',(0.,-1.22464679914735E-16,1.));
#6882=DIRECTION('ref_axis',(-2.22044604925031E-16,1.,1.22464679914735E-16));
#6883=DIRECTION('',(2.43604851491926E-16,-0.707106781186546,-0.707106781186549));
#6884=DIRECTION('center_axis',(0.,-1.22464679914735E-16,1.));
#6885=DIRECTION('ref_axis',(-2.22044604925031E-16,1.,1.22464679914735E-16));
#6886=DIRECTION('',(0.,-1.22464679914735E-16,1.));
#6887=DIRECTION('center_axis',(0.,1.22464679914735E-16,-1.));
#6888=DIRECTION('ref_axis',(1.,0.,0.));
#6889=DIRECTION('center_axis',(0.,-1.22464679914735E-16,1.));
#6890=DIRECTION('ref_axis',(1.,0.,0.));
#6891=DIRECTION('',(-0.707106781186548,-1.80858895911741E-32,-0.707106781186548));
#6892=DIRECTION('center_axis',(0.,1.22464679914735E-16,-1.));
#6893=DIRECTION('ref_axis',(1.,0.,0.));
#6894=DIRECTION('',(0.,-1.22464679914735E-16,1.));
#6895=DIRECTION('center_axis',(0.,1.22464679914735E-16,-1.));
#6896=DIRECTION('ref_axis',(1.,0.,0.));
#6897=DIRECTION('',(0.707106781186546,-1.73191211247099E-16,0.707106781186549));
#6898=DIRECTION('center_axis',(0.,-1.22464679914735E-16,1.));
#6899=DIRECTION('ref_axis',(1.,0.,0.));
#6900=DIRECTION('center_axis',(0.,1.22464679914735E-16,-1.));
#6901=DIRECTION('ref_axis',(1.,0.,0.));
#6902=DIRECTION('',(0.,-1.22464679914735E-16,1.));
#6903=DIRECTION('center_axis',(0.,-1.22464679914735E-16,1.));
#6904=DIRECTION('ref_axis',(-2.22044604925031E-16,1.,1.22464679914735E-16));
#6905=DIRECTION('',(0.,-1.22464679914735E-16,1.));
#6906=DIRECTION('center_axis',(0.,1.22464679914735E-16,-1.));
#6907=DIRECTION('ref_axis',(1.,0.,0.));
#6908=DIRECTION('',(0.,-1.22464679914735E-16,1.));
#6909=DIRECTION('center_axis',(0.,1.22464679914735E-16,-1.));
#6910=DIRECTION('ref_axis',(0.12166019715201,0.992571809205225,1.21554988906708E-16));
#7795=CARTESIAN_POINT('',(0.,0.,0.));
#7796=CARTESIAN_POINT('Origin',(-12.2859120418715,26.4797187186996,19.));
#7797=CARTESIAN_POINT('',(-12.2859120418715,26.4797187186996,19.));
#7798=CARTESIAN_POINT('',(-12.2859120418715,27.5976499618322,19.));
#7799=CARTESIAN_POINT('',(-12.2859120418715,25.4649312716304,19.));
#7800=CARTESIAN_POINT('',(-12.2859120418715,26.4797187186996,16.5));
#7801=CARTESIAN_POINT('',(-12.2859120418715,26.4797187186996,19.));
#7802=CARTESIAN_POINT('',(-12.2859120418715,27.5976499618322,16.5));
#7803=CARTESIAN_POINT('',(-12.2859120418715,26.4797187186996,16.5));
#7804=CARTESIAN_POINT('',(-12.2859120418715,27.5976499618322,19.));
#7805=CARTESIAN_POINT('Origin',(-10.8659120418715,25.1004782148047,19.));
#7806=CARTESIAN_POINT('',(-12.2859120418715,23.7212377109099,19.));
#7807=CARTESIAN_POINT('Origin',(-10.8659120418715,25.1004782148047,19.));
#7808=CARTESIAN_POINT('',(-12.2859120418715,23.7212377109099,16.5));
#7809=CARTESIAN_POINT('',(-12.2859120418715,23.7212377109099,19.));
#7810=CARTESIAN_POINT('Origin',(-10.8659120418715,25.1004782148047,16.5));
#7811=CARTESIAN_POINT('Origin',(-12.2859120418715,22.6033064677773,19.));
#7812=CARTESIAN_POINT('',(-12.2859120418715,22.6033064677773,19.));
#7813=CARTESIAN_POINT('',(-12.2859120418715,23.5267251461693,19.));
#7814=CARTESIAN_POINT('',(-12.2859120418715,22.6033064677773,16.5));
#7815=CARTESIAN_POINT('',(-12.2859120418715,22.6033064677773,19.));
#7816=CARTESIAN_POINT('',(-12.2859120418715,22.6033064677773,16.5));
#7817=CARTESIAN_POINT('Origin',(-10.8359120418715,22.6033064677773,19.));
#7818=CARTESIAN_POINT('',(-9.3859120418715,22.6033064677773,19.));
#7819=CARTESIAN_POINT('Origin',(-10.8359120418715,22.6033064677773,19.));
#7820=CARTESIAN_POINT('',(-9.3859120418715,22.6033064677773,16.5));
#7821=CARTESIAN_POINT('',(-9.3859120418715,22.6033064677773,19.));
#7822=CARTESIAN_POINT('Origin',(-10.8359120418715,22.6033064677773,16.5));
#7823=CARTESIAN_POINT('Origin',(-9.3859120418715,23.7858283117567,19.));
#7824=CARTESIAN_POINT('',(-9.3859120418715,23.7858283117567,19.));
#7825=CARTESIAN_POINT('',(-9.3859120418715,24.117986068159,19.));
#7826=CARTESIAN_POINT('',(-9.3859120418715,23.7858283117567,16.5));
#7827=CARTESIAN_POINT('',(-9.3859120418715,23.7858283117567,19.));
#7828=CARTESIAN_POINT('',(-9.3859120418715,23.7858283117567,16.5));
#7829=CARTESIAN_POINT('Origin',(-10.8659120418715,25.1004782148047,19.));
#7830=CARTESIAN_POINT('',(-9.3859120418715,26.4151281178527,19.));
#7831=CARTESIAN_POINT('Origin',(-10.8659120418715,25.1004782148047,19.));
#7832=CARTESIAN_POINT('',(-9.3859120418715,26.4151281178527,16.5));
#7833=CARTESIAN_POINT('',(-9.3859120418715,26.4151281178527,19.));
#7834=CARTESIAN_POINT('Origin',(-10.8659120418715,25.1004782148047,16.5));
#7835=CARTESIAN_POINT('Origin',(-9.3859120418715,27.5976499618322,19.));
#7836=CARTESIAN_POINT('',(-9.3859120418715,27.5976499618322,19.));
#7837=CARTESIAN_POINT('',(-9.38591204187149,26.0238968931967,19.));
#7838=CARTESIAN_POINT('',(-9.3859120418715,27.5976499618322,16.5));
#7839=CARTESIAN_POINT('',(-9.3859120418715,27.5976499618322,19.));
#7840=CARTESIAN_POINT('',(-9.3859120418715,27.5976499618322,16.5));
#7841=CARTESIAN_POINT('Origin',(-10.8359120418715,27.5976499618322,19.));
#7842=CARTESIAN_POINT('Origin',(-10.8359120418715,27.5976499618322,19.));
#7843=CARTESIAN_POINT('Origin',(-10.8359120418715,27.5976499618322,16.5));
#7844=CARTESIAN_POINT('Origin',(-6.27876228909014,17.7140879581285,19.));
#7845=CARTESIAN_POINT('',(-6.27876228909014,17.7140879581285,19.));
#7846=CARTESIAN_POINT('',(-7.39669353222272,17.7140879581285,19.));
#7847=CARTESIAN_POINT('',(-10.9854572864952,17.7140879581285,19.));
#7848=CARTESIAN_POINT('',(-6.27876228909014,17.7140879581285,16.5));
#7849=CARTESIAN_POINT('',(-6.27876228909014,17.7140879581285,19.));
#7850=CARTESIAN_POINT('',(-7.39669353222272,17.7140879581285,16.5));
#7851=CARTESIAN_POINT('',(-6.27876228909014,17.7140879581285,16.5));
#7852=CARTESIAN_POINT('',(-7.39669353222272,17.7140879581285,19.));
#7853=CARTESIAN_POINT('Origin',(-4.89952178519528,19.1340879581285,19.));
#7854=CARTESIAN_POINT('',(-3.52028128130042,17.7140879581285,19.));
#7855=CARTESIAN_POINT('Origin',(-4.89952178519528,19.1340879581285,19.));
#7856=CARTESIAN_POINT('',(-3.52028128130042,17.7140879581285,16.5));
#7857=CARTESIAN_POINT('',(-3.52028128130042,17.7140879581285,19.));
#7858=CARTESIAN_POINT('Origin',(-4.89952178519528,19.1340879581285,16.5));
#7859=CARTESIAN_POINT('Origin',(-2.40235003816785,17.7140879581285,19.));
#7860=CARTESIAN_POINT('',(-2.40235003816785,17.7140879581285,19.));
#7861=CARTESIAN_POINT('',(-9.04725116103404,17.7140879581285,19.));
#7862=CARTESIAN_POINT('',(-2.40235003816785,17.7140879581285,16.5));
#7863=CARTESIAN_POINT('',(-2.40235003816785,17.7140879581285,19.));
#7864=CARTESIAN_POINT('',(-2.40235003816785,17.7140879581285,16.5));
#7865=CARTESIAN_POINT('Origin',(-2.40235003816784,19.1640879581285,19.));
#7866=CARTESIAN_POINT('',(-2.40235003816784,20.6140879581285,19.));
#7867=CARTESIAN_POINT('Origin',(-2.40235003816784,19.1640879581285,19.));
#7868=CARTESIAN_POINT('',(-2.40235003816784,20.6140879581285,16.5));
#7869=CARTESIAN_POINT('',(-2.40235003816784,20.6140879581285,19.));
#7870=CARTESIAN_POINT('Origin',(-2.40235003816784,19.1640879581285,16.5));
#7871=CARTESIAN_POINT('Origin',(-3.58487188214727,20.6140879581285,19.));
#7872=CARTESIAN_POINT('',(-3.58487188214727,20.6140879581285,19.));
#7873=CARTESIAN_POINT('',(-9.63851208302377,20.6140879581286,19.));
#7874=CARTESIAN_POINT('',(-3.58487188214727,20.6140879581285,16.5));
#7875=CARTESIAN_POINT('',(-3.58487188214727,20.6140879581285,19.));
#7876=CARTESIAN_POINT('',(-3.58487188214727,20.6140879581285,16.5));
#7877=CARTESIAN_POINT('Origin',(-4.89952178519528,19.1340879581285,19.));
#7878=CARTESIAN_POINT('',(-6.21417168824329,20.6140879581285,19.));
#7879=CARTESIAN_POINT('Origin',(-4.89952178519528,19.1340879581285,19.));
#7880=CARTESIAN_POINT('',(-6.21417168824329,20.6140879581285,16.5));
#7881=CARTESIAN_POINT('',(-6.21417168824329,20.6140879581285,19.));
#7882=CARTESIAN_POINT('Origin',(-4.89952178519528,19.1340879581285,16.5));
#7883=CARTESIAN_POINT('Origin',(-7.39669353222272,20.6140879581285,19.));
#7884=CARTESIAN_POINT('',(-7.39669353222272,20.6140879581285,19.));
#7885=CARTESIAN_POINT('',(-11.5444229080615,20.6140879581285,19.));
#7886=CARTESIAN_POINT('',(-7.39669353222272,20.6140879581285,16.5));
#7887=CARTESIAN_POINT('',(-7.39669353222272,20.6140879581285,19.));
#7888=CARTESIAN_POINT('',(-7.39669353222272,20.6140879581285,16.5));
#7889=CARTESIAN_POINT('Origin',(-7.39669353222272,19.1640879581285,19.));
#7890=CARTESIAN_POINT('Origin',(-7.39669353222272,19.1640879581285,19.));
#7891=CARTESIAN_POINT('Origin',(-7.39669353222272,19.1640879581285,16.5));
#7892=CARTESIAN_POINT('Origin',(-17.2859120418715,27.5976499618322,19.));
#7893=CARTESIAN_POINT('',(-17.2859120418715,27.5976499618322,19.));
#7894=CARTESIAN_POINT('',(-17.2859120418715,26.4481444819436,19.));
#7895=CARTESIAN_POINT('',(-17.2859120418715,26.0238968931967,19.));
#7896=CARTESIAN_POINT('',(-17.2859120418715,27.5976499618322,16.5));
#7897=CARTESIAN_POINT('',(-17.2859120418715,27.5976499618322,19.));
#7898=CARTESIAN_POINT('',(-17.2859120418715,26.4481444819436,16.5));
#7899=CARTESIAN_POINT('',(-17.2859120418715,27.5976499618322,16.5));
#7900=CARTESIAN_POINT('',(-17.2859120418715,26.4481444819436,19.));
#7901=CARTESIAN_POINT('Origin',(-18.7359120418715,27.5976499618322,19.));
#7902=CARTESIAN_POINT('',(-20.1859120418715,27.5976499618322,19.));
#7903=CARTESIAN_POINT('Origin',(-18.7359120418715,27.5976499618322,19.));
#7904=CARTESIAN_POINT('',(-20.1859120418715,27.5976499618322,16.5));
#7905=CARTESIAN_POINT('',(-20.1859120418715,27.5976499618322,19.));
#7906=CARTESIAN_POINT('Origin',(-18.7359120418715,27.5976499618322,16.5));
#7907=CARTESIAN_POINT('Origin',(-20.1859120418715,26.4481444819436,19.));
#7908=CARTESIAN_POINT('',(-20.1859120418715,26.4481444819436,19.));
#7909=CARTESIAN_POINT('',(-20.1859120418715,25.4491441532525,19.));
#7910=CARTESIAN_POINT('',(-20.1859120418715,26.4481444819436,16.5));
#7911=CARTESIAN_POINT('',(-20.1859120418715,26.4481444819436,19.));
#7912=CARTESIAN_POINT('',(-20.1859120418715,26.4481444819436,16.5));
#7913=CARTESIAN_POINT('Origin',(-18.7359120418715,25.1004782148047,19.));
#7914=CARTESIAN_POINT('',(-20.1859120418715,23.7528119476658,19.));
#7915=CARTESIAN_POINT('Origin',(-18.7359120418715,25.1004782148047,19.));
#7916=CARTESIAN_POINT('',(-20.1859120418715,23.7528119476658,16.5));
#7917=CARTESIAN_POINT('',(-20.1859120418715,23.7528119476658,19.));
#7918=CARTESIAN_POINT('Origin',(-18.7359120418715,25.1004782148047,16.5));
#7919=CARTESIAN_POINT('Origin',(-20.1859120418715,22.6033064677773,19.));
#7920=CARTESIAN_POINT('',(-20.1859120418715,22.6033064677773,19.));
#7921=CARTESIAN_POINT('',(-20.1859120418715,23.5267251461693,19.));
#7922=CARTESIAN_POINT('',(-20.1859120418715,22.6033064677773,16.5));
#7923=CARTESIAN_POINT('',(-20.1859120418715,22.6033064677773,19.));
#7924=CARTESIAN_POINT('',(-20.1859120418715,22.6033064677773,16.5));
#7925=CARTESIAN_POINT('Origin',(-18.7359120418715,22.6033064677773,19.));
#7926=CARTESIAN_POINT('',(-17.2859120418715,22.6033064677773,19.));
#7927=CARTESIAN_POINT('Origin',(-18.7359120418715,22.6033064677773,19.));
#7928=CARTESIAN_POINT('',(-17.2859120418715,22.6033064677773,16.5));
#7929=CARTESIAN_POINT('',(-17.2859120418715,22.6033064677773,19.));
#7930=CARTESIAN_POINT('Origin',(-18.7359120418715,22.6033064677773,16.5));
#7931=CARTESIAN_POINT('Origin',(-17.2859120418715,23.7528119476658,19.));
#7932=CARTESIAN_POINT('',(-17.2859120418715,23.7528119476658,19.));
#7933=CARTESIAN_POINT('',(-17.2859120418715,24.1014778861135,19.));
#7934=CARTESIAN_POINT('',(-17.2859120418715,23.7528119476658,16.5));
#7935=CARTESIAN_POINT('',(-17.2859120418715,23.7528119476658,19.));
#7936=CARTESIAN_POINT('',(-17.2859120418715,23.7528119476658,16.5));
#7937=CARTESIAN_POINT('Origin',(-18.7359120418715,25.1004782148047,19.));
#7938=CARTESIAN_POINT('Origin',(-18.7359120418715,25.1004782148047,19.));
#7939=CARTESIAN_POINT('Origin',(-18.7359120418715,25.1004782148047,16.5));
#7940=CARTESIAN_POINT('Origin',(-3.55185551805636,12.7140879581285,19.));
#7941=CARTESIAN_POINT('',(-3.55185551805636,12.7140879581285,19.));
#7942=CARTESIAN_POINT('',(-2.40235003816785,12.7140879581285,19.));
#7943=CARTESIAN_POINT('',(-9.6220039009783,12.7140879581285,19.));
#7944=CARTESIAN_POINT('',(-3.55185551805636,12.7140879581285,16.5));
#7945=CARTESIAN_POINT('',(-3.55185551805636,12.7140879581285,19.));
#7946=CARTESIAN_POINT('',(-2.40235003816785,12.7140879581285,16.5));
#7947=CARTESIAN_POINT('',(-3.55185551805636,12.7140879581285,16.5));
#7948=CARTESIAN_POINT('',(-2.40235003816785,12.7140879581285,19.));
#7949=CARTESIAN_POINT('Origin',(-4.89952178519528,11.2640879581285,19.));
#7950=CARTESIAN_POINT('',(-6.2471880523342,12.7140879581285,19.));
#7951=CARTESIAN_POINT('Origin',(-4.89952178519528,11.2640879581285,19.));
#7952=CARTESIAN_POINT('',(-6.2471880523342,12.7140879581285,16.5));
#7953=CARTESIAN_POINT('',(-6.2471880523342,12.7140879581285,19.));
#7954=CARTESIAN_POINT('Origin',(-4.89952178519528,11.2640879581285,16.5));
#7955=CARTESIAN_POINT('Origin',(-7.39669353222271,12.7140879581285,19.));
#7956=CARTESIAN_POINT('',(-7.39669353222271,12.7140879581285,19.));
#7957=CARTESIAN_POINT('',(-11.5444229080615,12.7140879581285,19.));
#7958=CARTESIAN_POINT('',(-7.39669353222271,12.7140879581285,16.5));
#7959=CARTESIAN_POINT('',(-7.39669353222271,12.7140879581285,19.));
#7960=CARTESIAN_POINT('',(-7.39669353222271,12.7140879581285,16.5));
#7961=CARTESIAN_POINT('Origin',(-7.39669353222271,11.2640879581285,19.));
#7962=CARTESIAN_POINT('',(-7.39669353222271,9.8140879581285,19.));
#7963=CARTESIAN_POINT('Origin',(-7.39669353222271,11.2640879581285,19.));
#7964=CARTESIAN_POINT('',(-7.39669353222271,9.8140879581285,16.5));
#7965=CARTESIAN_POINT('',(-7.39669353222271,9.8140879581285,19.));
#7966=CARTESIAN_POINT('Origin',(-7.39669353222271,11.2640879581285,16.5));
#7967=CARTESIAN_POINT('Origin',(-6.2471880523342,9.8140879581285,19.));
#7968=CARTESIAN_POINT('',(-6.2471880523342,9.8140879581285,19.));
#7969=CARTESIAN_POINT('',(-10.9696701681172,9.8140879581285,19.));
#7970=CARTESIAN_POINT('',(-6.2471880523342,9.8140879581285,16.5));
#7971=CARTESIAN_POINT('',(-6.2471880523342,9.8140879581285,19.));
#7972=CARTESIAN_POINT('',(-6.2471880523342,9.8140879581285,16.5));
#7973=CARTESIAN_POINT('Origin',(-4.89952178519528,11.2640879581285,19.));
#7974=CARTESIAN_POINT('',(-3.55185551805636,9.8140879581285,19.));
#7975=CARTESIAN_POINT('Origin',(-4.89952178519528,11.2640879581285,19.));
#7976=CARTESIAN_POINT('',(-3.55185551805636,9.8140879581285,16.5));
#7977=CARTESIAN_POINT('',(-3.55185551805636,9.8140879581285,19.));
#7978=CARTESIAN_POINT('Origin',(-4.89952178519528,11.2640879581285,16.5));
#7979=CARTESIAN_POINT('Origin',(-2.40235003816785,9.8140879581285,19.));
#7980=CARTESIAN_POINT('',(-2.40235003816785,9.8140879581285,19.));
#7981=CARTESIAN_POINT('',(-9.04725116103404,9.8140879581285,19.));
#7982=CARTESIAN_POINT('',(-2.40235003816785,9.8140879581285,16.5));
#7983=CARTESIAN_POINT('',(-2.40235003816785,9.8140879581285,19.));
#7984=CARTESIAN_POINT('',(-2.40235003816785,9.8140879581285,16.5));
#7985=CARTESIAN_POINT('Origin',(-2.40235003816785,11.2640879581285,19.));
#7986=CARTESIAN_POINT('Origin',(-2.40235003816785,11.2640879581285,19.));
#7987=CARTESIAN_POINT('Origin',(-2.40235003816785,11.2640879581285,16.5));
#7988=CARTESIAN_POINT('Origin',(-10.8659120418715,25.1004782148047,19.));
#7989=CARTESIAN_POINT('',(-12.6454838055578,25.1004782148047,8.6));
#7990=CARTESIAN_POINT('Origin',(-10.8659120418715,25.1004782148047,8.6));
#7991=CARTESIAN_POINT('',(-12.6454838055578,25.1004782148047,16.5));
#7992=CARTESIAN_POINT('',(-12.6454838055578,25.1004782148047,19.));
#7993=CARTESIAN_POINT('Origin',(-10.8659120418715,25.1004782148047,16.5));
#7994=CARTESIAN_POINT('Origin',(-4.89952178519528,11.2640879581285,19.));
#7995=CARTESIAN_POINT('',(-4.89952178519528,9.48451619444218,8.6));
#7996=CARTESIAN_POINT('Origin',(-4.89952178519528,11.2640879581285,8.6));
#7997=CARTESIAN_POINT('',(-4.89952178519528,9.48451619444219,16.5));
#7998=CARTESIAN_POINT('',(-4.89952178519528,9.48451619444219,19.));
#7999=CARTESIAN_POINT('Origin',(-4.89952178519528,11.2640879581285,16.5));
#8000=CARTESIAN_POINT('Origin',(-15.0254707357525,14.9637210836027,8.85));
#8001=CARTESIAN_POINT('',(-11.0997123508774,18.9002876491226,9.1));
#8002=CARTESIAN_POINT('',(-10.7461586545955,19.2538413470203,8.6));
#8003=CARTESIAN_POINT('Ctrl Pts',(-11.0997123508774,18.9002876491226,9.1));
#8004=CARTESIAN_POINT('Ctrl Pts',(-11.0702528871568,18.9297537969895,9.05833333333333));
#8005=CARTESIAN_POINT('Ctrl Pts',(-11.0407925873132,18.9592191099766,9.01666666666666));
#8006=CARTESIAN_POINT('Ctrl Pts',(-10.9818703154508,19.0181480661202,8.93333333333333));
#8007=CARTESIAN_POINT('Ctrl Pts',(-10.952408343432,19.0476117092766,8.89166666666666));
#8008=CARTESIAN_POINT('Ctrl Pts',(-10.8934827272903,19.1065373256877,8.80833333333333));
#8009=CARTESIAN_POINT('Ctrl Pts',(-10.8640190831674,19.1359992989424,8.76666666666667));
#8010=CARTESIAN_POINT('Ctrl Pts',(-10.8050901228885,19.1949215754788,8.68333333333333));
#8011=CARTESIAN_POINT('Ctrl Pts',(-10.7756248067326,19.2243818787606,8.64166666666666));
#8012=CARTESIAN_POINT('Ctrl Pts',(-10.7461586545955,19.2538413470203,8.6));
#8013=CARTESIAN_POINT('',(-8.96603335068975,14.9343554740278,8.6));
#8014=CARTESIAN_POINT('Origin',(-15.0254707357525,14.9637210836027,8.6));
#8015=CARTESIAN_POINT('',(-9.46602747923395,14.9367785756188,9.1));
#8016=CARTESIAN_POINT('',(-8.96603335068975,14.9343554740278,8.6));
#8017=CARTESIAN_POINT('Origin',(-15.0254707357525,14.9637210836027,9.1));
#8018=CARTESIAN_POINT('Origin',(90.5327982296072,14.4521582574094,8.85));
#8019=CARTESIAN_POINT('',(-8.96720177039285,14.4521582574094,8.6));
#8020=CARTESIAN_POINT('',(-9.46720177039287,14.4521582574094,9.1));
#8021=CARTESIAN_POINT('',(-8.96720177039285,14.4521582574094,8.6));
#8022=CARTESIAN_POINT('Origin',(90.5327982296072,14.4521582574094,9.1));
#8023=CARTESIAN_POINT('Origin',(90.5327982296072,14.4521582574094,8.6));
#8024=CARTESIAN_POINT('Origin',(-9.21720177039288,19.6482354995058,8.85));
#8025=CARTESIAN_POINT('',(-8.96720177039288,9.34727392485797,8.6));
#8026=CARTESIAN_POINT('',(-9.46720177039288,9.34727392485797,9.1));
#8027=CARTESIAN_POINT('',(-8.96720177039288,9.34727392485797,8.6));
#8028=CARTESIAN_POINT('',(-9.46720177039288,19.6482354995058,9.1));
#8029=CARTESIAN_POINT('',(-8.96720177039288,19.6482354995058,8.6));
#8030=CARTESIAN_POINT('Origin',(-7.9672017703919,9.34727392485799,8.85));
#8031=CARTESIAN_POINT('',(-8.96519438024848,9.28394343714784,8.6));
#8032=CARTESIAN_POINT('',(-9.46419068517628,9.2522781932928,9.1));
#8033=CARTESIAN_POINT('',(-8.96519438024848,9.28394343714784,8.6));
#8034=CARTESIAN_POINT('Origin',(-7.9672017703919,9.34727392485799,9.1));
#8035=CARTESIAN_POINT('Origin',(-7.9672017703919,9.34727392485799,8.6));
#8036=CARTESIAN_POINT('Origin',(-9.70746000988541,17.0333802514339,8.85));
#8037=CARTESIAN_POINT('',(-8.5966084889616,3.47558779515293,8.6));
#8038=CARTESIAN_POINT('',(-9.0956047938894,3.44392255129787,9.1));
#8039=CARTESIAN_POINT('',(-8.5966084889616,3.47558779515293,8.6));
#8040=CARTESIAN_POINT('',(-9.95695816234931,17.0175476295063,9.1));
#8041=CARTESIAN_POINT('',(-9.45796185742151,17.0492128733614,8.6));
#8042=CARTESIAN_POINT('Origin',(-8.09761218403378,3.50725303900799,8.85));
#8043=CARTESIAN_POINT('',(-8.44775642389183,3.15032305806741,8.6));
#8044=CARTESIAN_POINT('',(-8.79790066374987,2.79339307712684,9.1));
#8045=CARTESIAN_POINT('',(-8.44775642389183,3.15032305806741,8.6));
#8046=CARTESIAN_POINT('Origin',(-8.09761218403378,3.50725303900799,9.1));
#8047=CARTESIAN_POINT('Origin',(-8.09761218403378,3.50725303900799,8.6));
#8048=CARTESIAN_POINT('Origin',(-15.7926606978681,10.0053816255599,8.85));
#8049=CARTESIAN_POINT('',(-6.36480204371692,1.10696857105172,8.6));
#8050=CARTESIAN_POINT('',(-6.71494628357496,0.750038590111153,9.1));
#8051=CARTESIAN_POINT('',(-6.36480204371692,1.10696857105172,8.6));
#8052=CARTESIAN_POINT('',(-15.9677328177972,9.82691663508957,9.1));
#8053=CARTESIAN_POINT('',(-15.6175885779391,10.1838466160301,8.6));
#8054=CARTESIAN_POINT('Origin',(-6.01465780385887,1.4638985519923,8.85));
#8055=CARTESIAN_POINT('',(-6.01465780385887,0.963898551992286,8.6));
#8056=CARTESIAN_POINT('',(-6.01465780385888,0.463898551992283,9.1));
#8057=CARTESIAN_POINT('',(-6.01465780385887,0.963898551992286,8.6));
#8058=CARTESIAN_POINT('Origin',(-6.01465780385887,1.4638985519923,9.1));
#8059=CARTESIAN_POINT('Origin',(-6.01465780385887,1.4638985519923,8.6));
#8060=CARTESIAN_POINT('Origin',(-10.8534050438796,0.713898551992282,8.85));
#8061=CARTESIAN_POINT('',(-3.77953774500221,0.963898551992282,8.6));
#8062=CARTESIAN_POINT('',(-3.77953774500221,0.463898551992283,9.1));
#8063=CARTESIAN_POINT('',(-3.77953774500221,0.963898551992282,8.6));
#8064=CARTESIAN_POINT('',(-10.8534050438796,0.463898551992283,9.1));
#8065=CARTESIAN_POINT('',(-10.8534050438796,0.963898551992282,8.6));
#8066=CARTESIAN_POINT('Origin',(-3.77953774500221,1.46389855199228,8.85));
#8067=CARTESIAN_POINT('',(-3.42509449740134,1.11123726374228,8.6));
#8068=CARTESIAN_POINT('',(-3.07065124980047,0.758575975492284,9.1));
#8069=CARTESIAN_POINT('',(-3.42509449740134,1.11123726374228,8.6));
#8070=CARTESIAN_POINT('Origin',(-3.77953774500221,1.46389855199228,9.1));
#8071=CARTESIAN_POINT('Origin',(-3.77953774500221,1.46389855199228,8.6));
#8072=CARTESIAN_POINT('Origin',(-0.464527910187313,3.73231552412535,8.85));
#8073=CARTESIAN_POINT('',(-1.31055213694564,3.23646417806756,8.6));
#8074=CARTESIAN_POINT('',(-0.956108889344776,2.88380288981756,9.1));
#8075=CARTESIAN_POINT('',(-1.31055213694564,3.23646417806756,8.6));
#8076=CARTESIAN_POINT('',(-0.28730628638688,3.55598488000036,9.1));
#8077=CARTESIAN_POINT('',(-0.641749533987747,3.90864616825035,8.6));
#8078=CARTESIAN_POINT('Origin',(-1.66499538454653,3.58912546631757,8.85));
#8079=CARTESIAN_POINT('',(-1.16813965229678,3.53313992058853,8.6));
#8080=CARTESIAN_POINT('',(-0.671283920047039,3.4771543748595,9.1));
#8081=CARTESIAN_POINT('',(-1.16813965229678,3.53313992058853,8.6));
#8082=CARTESIAN_POINT('Origin',(-1.66499538454653,3.58912546631757,9.1));
#8083=CARTESIAN_POINT('Origin',(-1.66499538454653,3.58912546631757,8.6));
#8084=CARTESIAN_POINT('Origin',(0.152926315598855,13.0245040201872,8.85));
#8085=CARTESIAN_POINT('',(-0.506288535500522,9.40687959739178,8.6));
#8086=CARTESIAN_POINT('',(-0.00943280325078496,9.35089405166274,9.1));
#8087=CARTESIAN_POINT('',(-0.506288535500522,9.40687959739178,8.6));
#8088=CARTESIAN_POINT('',(0.401354181723723,12.9965112473227,9.1));
#8089=CARTESIAN_POINT('',(-0.0955015505260137,13.0524967930517,8.6));
#8090=CARTESIAN_POINT('Origin',(-1.50000000000024,9.51885068884986,8.85));
#8091=CARTESIAN_POINT('',(-0.499999999999996,9.51885068884985,8.6));
#8092=CARTESIAN_POINT('',(4.4067824247818E-15,9.51885068884984,9.1));
#8093=CARTESIAN_POINT('',(-0.499999999999996,9.51885068884985,8.6));
#8094=CARTESIAN_POINT('Origin',(-1.50000000000024,9.51885068884986,9.1));
#8095=CARTESIAN_POINT('Origin',(-1.50000000000024,9.51885068884986,8.6));
#8096=CARTESIAN_POINT('Origin',(-0.249999999999997,16.9844972567056,8.85));
#8097=CARTESIAN_POINT('',(-0.499999999999998,20.4800179767447,8.6));
#8098=CARTESIAN_POINT('',(2.11386064724713E-15,20.4800179767447,9.1));
#8099=CARTESIAN_POINT('',(-0.499999999999998,20.4800179767447,8.6));
#8100=CARTESIAN_POINT('',(2.84494650060196E-15,16.9844972567056,9.1));
#8101=CARTESIAN_POINT('',(-0.499999999999997,16.9844972567056,8.6));
#8102=CARTESIAN_POINT('Origin',(-1.50000000000038,20.4800179767447,8.85));
#8103=CARTESIAN_POINT('',(-0.507428190794775,20.6016781738967,8.6));
#8104=CARTESIAN_POINT('',(-0.011142286192162,20.6625082724727,9.1));
#8105=CARTESIAN_POINT('',(-0.507428190794775,20.6016781738967,8.6));
#8106=CARTESIAN_POINT('Origin',(-1.50000000000038,20.4800179767447,9.1));
#8107=CARTESIAN_POINT('Origin',(-1.50000000000038,20.4800179767447,8.6));
#8108=CARTESIAN_POINT('Origin',(-0.604024921256996,23.4446720175285,8.85));
#8109=CARTESIAN_POINT('',(-1.11678107889193,25.5731192264483,8.6));
#8110=CARTESIAN_POINT('',(-0.620495174289325,25.6339493250243,9.1));
#8111=CARTESIAN_POINT('',(-1.11678107889193,25.5731192264483,8.6));
#8112=CARTESIAN_POINT('',(-0.355881968955691,23.4750870668165,9.1));
#8113=CARTESIAN_POINT('',(-0.8521678735583,23.4142569682405,8.6));
#8114=CARTESIAN_POINT('Origin',(-4.88927830720691,25.1107216927931,8.85));
#8115=CARTESIAN_POINT('',(-4.42688077355167,28.8832189211081,8.6));
#8116=CARTESIAN_POINT('Origin',(-4.88927830720691,25.1107216927931,8.6));
#8117=CARTESIAN_POINT('',(-4.36605067497567,29.3795048257107,9.1));
#8118=CARTESIAN_POINT('',(-4.42688077355167,28.8832189211081,8.6));
#8119=CARTESIAN_POINT('Origin',(-4.88927830720691,25.1107216927931,9.1));
#8120=CARTESIAN_POINT('Origin',(-12.1637909407195,30.0834081721396,8.85));
#8121=CARTESIAN_POINT('',(-9.39832182610329,29.4925718092052,8.6));
#8122=CARTESIAN_POINT('',(-12.1942059900075,29.8352652198383,8.6));
#8123=CARTESIAN_POINT('',(-9.33749172752729,29.9888577138078,9.1));
#8124=CARTESIAN_POINT('',(-9.39832182610329,29.4925718092052,8.6));
#8125=CARTESIAN_POINT('',(-12.1333758914315,30.3315511244409,9.1));
#8126=CARTESIAN_POINT('Origin',(-9.51998202325534,28.4999999999996,8.85));
#8127=CARTESIAN_POINT('',(-9.51998202325534,29.5,8.6));
#8128=CARTESIAN_POINT('Origin',(-9.51998202325534,28.4999999999996,8.6));
#8129=CARTESIAN_POINT('',(-9.51998202325534,30.,9.1));
#8130=CARTESIAN_POINT('',(-9.51998202325534,29.5,8.6));
#8131=CARTESIAN_POINT('Origin',(-9.51998202325534,28.4999999999996,9.1));
#8132=CARTESIAN_POINT('Origin',(-18.0866507975252,29.75,8.85));
#8133=CARTESIAN_POINT('',(-20.4811493111502,29.5,8.6));
#8134=CARTESIAN_POINT('',(-18.0866507975252,29.5,8.6));
#8135=CARTESIAN_POINT('',(-20.4811493111502,30.,9.1));
#8136=CARTESIAN_POINT('',(-20.4811493111502,29.5,8.6));
#8137=CARTESIAN_POINT('',(-18.0866507975252,30.,9.1));
#8138=CARTESIAN_POINT('Origin',(-20.4811493111501,28.4999999999997,8.85));
#8139=CARTESIAN_POINT('',(-20.5931204026082,29.4937114644995,8.6));
#8140=CARTESIAN_POINT('Origin',(-20.4811493111501,28.4999999999998,8.6));
#8141=CARTESIAN_POINT('',(-20.6491059483372,29.9905671967492,9.1));
#8142=CARTESIAN_POINT('',(-20.5931204026082,29.4937114644995,8.6));
#8143=CARTESIAN_POINT('Origin',(-20.4811493111501,28.4999999999997,9.1));
#8144=CARTESIAN_POINT('Origin',(-21.4188131730182,29.6522547488597,8.85));
#8145=CARTESIAN_POINT('',(-26.4668600794115,28.8318603477032,8.6));
#8146=CARTESIAN_POINT('',(-21.3908204001537,29.4038268827348,8.6));
#8147=CARTESIAN_POINT('',(-26.5228456251405,29.328716079953,9.1));
#8148=CARTESIAN_POINT('',(-26.4668600794115,28.8318603477032,8.6));
#8149=CARTESIAN_POINT('',(-21.4468059458827,29.9006826149846,9.1));
#8150=CARTESIAN_POINT('Origin',(-26.4108745336824,28.3350046154535,8.85));
#8151=CARTESIAN_POINT('',(-26.7635358219324,28.6894478630543,8.6));
#8152=CARTESIAN_POINT('Origin',(-26.4108745336824,28.3350046154535,8.6));
#8153=CARTESIAN_POINT('',(-27.1161971101824,29.0438911106552,9.1));
#8154=CARTESIAN_POINT('',(-26.7635358219324,28.6894478630543,8.6));
#8155=CARTESIAN_POINT('Origin',(-26.4108745336824,28.3350046154535,9.1));
#8156=CARTESIAN_POINT('Origin',(-26.2804962944917,29.5227246824664,8.85));
#8157=CARTESIAN_POINT('',(-28.8887627362577,26.5749055025987,8.6));
#8158=CARTESIAN_POINT('',(-26.1041656503667,29.345503058666,8.6));
#8159=CARTESIAN_POINT('',(-29.2414240245077,26.9293487501995,9.1));
#8160=CARTESIAN_POINT('',(-28.8887627362577,26.5749055025987,8.6));
#8161=CARTESIAN_POINT('',(-26.4568269386167,29.6999463062668,9.1));
#8162=CARTESIAN_POINT('Origin',(-28.5361014480077,26.2204622549978,8.85));
#8163=CARTESIAN_POINT('',(-29.0361014480077,26.2204622549978,8.6));
#8164=CARTESIAN_POINT('Origin',(-28.5361014480077,26.2204622549978,8.6));
#8165=CARTESIAN_POINT('',(-29.5361014480077,26.2204622549978,9.1));
#8166=CARTESIAN_POINT('',(-29.0361014480077,26.2204622549978,8.6));
#8167=CARTESIAN_POINT('Origin',(-28.5361014480077,26.2204622549978,9.1));
#8168=CARTESIAN_POINT('Origin',(-29.2861014480077,24.2177430103512,8.85));
#8169=CARTESIAN_POINT('',(-29.0361014480077,23.9853421961411,8.6));
#8170=CARTESIAN_POINT('',(-29.0361014480077,24.2177430103512,8.6));
#8171=CARTESIAN_POINT('',(-29.5361014480077,23.9853421961411,9.1));
#8172=CARTESIAN_POINT('',(-29.0361014480077,23.9853421961411,8.6));
#8173=CARTESIAN_POINT('',(-29.5361014480077,24.2177430103512,9.1));
#8174=CARTESIAN_POINT('Origin',(-28.5361014480077,23.9853421961411,8.85));
#8175=CARTESIAN_POINT('',(-28.8930314289483,23.6351979562831,8.6));
#8176=CARTESIAN_POINT('Origin',(-28.5361014480077,23.9853421961411,8.6));
#8177=CARTESIAN_POINT('',(-29.2499614098888,23.285053716425,9.1));
#8178=CARTESIAN_POINT('',(-28.8930314289483,23.6351979562831,8.6));
#8179=CARTESIAN_POINT('Origin',(-28.5361014480077,23.9853421961411,9.1));
#8180=CARTESIAN_POINT('Origin',(-25.0166364478165,19.3266833071628,8.85));
#8181=CARTESIAN_POINT('',(-26.8496769419326,21.5522435761082,8.6));
#8182=CARTESIAN_POINT('',(-24.8381714573462,19.5017554270918,8.6));
#8183=CARTESIAN_POINT('',(-27.2066069228731,21.2020993362501,9.1));
#8184=CARTESIAN_POINT('',(-26.8496769419326,21.5522435761082,8.6));
#8185=CARTESIAN_POINT('',(-25.1951014382868,19.1516111872338,9.1));
#8186=CARTESIAN_POINT('Origin',(-26.492746960992,21.9023878159662,8.85));
#8187=CARTESIAN_POINT('',(-26.5244122048471,21.4033915110384,8.6));
#8188=CARTESIAN_POINT('Origin',(-26.492746960992,21.9023878159662,8.6));
#8189=CARTESIAN_POINT('',(-26.5560774487021,20.9043952061106,9.1));
#8190=CARTESIAN_POINT('',(-26.5244122048471,21.4033915110384,8.6));
#8191=CARTESIAN_POINT('Origin',(-26.492746960992,21.9023878159662,9.1));
#8192=CARTESIAN_POINT('Origin',(-18.337942281882,20.6333926901486,8.85));
#8193=CARTESIAN_POINT('',(-20.7160565628521,21.0348056197515,8.6));
#8194=CARTESIAN_POINT('',(-18.3221096599545,20.8828908426125,8.6));
#8195=CARTESIAN_POINT('',(-20.7477218067072,20.5358093148237,9.1));
#8196=CARTESIAN_POINT('',(-20.7160565628521,21.0348056197515,8.6));
#8197=CARTESIAN_POINT('',(-18.3537749038095,20.3838945376847,9.1));
#8198=CARTESIAN_POINT('Origin',(-20.652726075142,22.0327982296081,8.85));
#8199=CARTESIAN_POINT('',(-20.652726075142,21.0327982296071,8.6));
#8200=CARTESIAN_POINT('Origin',(-20.652726075142,22.0327982296081,8.6));
#8201=CARTESIAN_POINT('',(-20.652726075142,20.5327982296071,9.1));
#8202=CARTESIAN_POINT('',(-20.652726075142,21.0327982296071,8.6));
#8203=CARTESIAN_POINT('Origin',(-20.652726075142,22.0327982296081,9.1));
#8204=CARTESIAN_POINT('Origin',(-15.4229125547249,20.7827982296071,8.85));
#8205=CARTESIAN_POINT('',(-15.5478417425962,21.0327982296071,8.6));
#8206=CARTESIAN_POINT('',(-15.4229125547249,21.0327982296071,8.6));
#8207=CARTESIAN_POINT('',(-15.5478417425962,20.5327982296071,9.1));
#8208=CARTESIAN_POINT('',(-15.5478417425962,21.0327982296071,8.6));
#8209=CARTESIAN_POINT('',(-15.4229125547249,20.5327982296071,9.1));
#8210=CARTESIAN_POINT('Origin',(-15.5478417425962,120.532798229607,8.85000000000001));
#8211=CARTESIAN_POINT('',(-15.0656445259725,21.0339666493103,8.6));
#8212=CARTESIAN_POINT('',(-15.0632214243815,20.533972520766,9.1));
#8213=CARTESIAN_POINT('',(-15.0656445259725,21.0339666493103,8.6));
#8214=CARTESIAN_POINT('Origin',(-15.5478417425962,120.532798229607,9.10000000000001));
#8215=CARTESIAN_POINT('Origin',(-15.5478417425962,120.532798229607,8.60000000000001));
#8216=CARTESIAN_POINT('Origin',(-15.0362789163973,14.9745292642475,8.85));
#8217=CARTESIAN_POINT('Origin',(-15.0362789163973,14.9745292642475,9.1));
#8218=CARTESIAN_POINT('Origin',(-15.0362789163973,14.9745292642475,8.6));
#8219=CARTESIAN_POINT('Origin',(-9.33749172752729,29.9888577138078,19.));
#8220=CARTESIAN_POINT('',(-9.33749172752729,29.9888577138078,18.5));
#8221=CARTESIAN_POINT('',(-9.33749172752729,29.9888577138078,19.));
#8222=CARTESIAN_POINT('',(-4.36605067497567,29.3795048257107,18.5));
#8223=CARTESIAN_POINT('',(-12.1333758914315,30.3315511244409,18.5));
#8224=CARTESIAN_POINT('',(-4.36605067497567,29.3795048257107,19.));
#8225=CARTESIAN_POINT('Origin',(-9.51998202325534,28.4999999999996,19.));
#8226=CARTESIAN_POINT('',(-9.51998202325534,30.,18.5));
#8227=CARTESIAN_POINT('',(-9.51998202325534,30.,19.));
#8228=CARTESIAN_POINT('Origin',(-9.51998202325534,28.4999999999996,18.5));
#8229=CARTESIAN_POINT('Origin',(-20.4811493111501,30.,19.));
#8230=CARTESIAN_POINT('',(-20.4811493111502,30.,18.5));
#8231=CARTESIAN_POINT('',(-20.4811493111502,30.,19.));
#8232=CARTESIAN_POINT('',(-18.0866507975252,30.,18.5));
#8233=CARTESIAN_POINT('Origin',(-20.4811493111501,28.4999999999997,19.));
#8234=CARTESIAN_POINT('',(-20.6491059483372,29.9905671967492,18.5));
#8235=CARTESIAN_POINT('',(-20.6491059483372,29.9905671967492,19.));
#8236=CARTESIAN_POINT('Origin',(-20.4811493111501,28.4999999999997,18.5));
#8237=CARTESIAN_POINT('Origin',(-26.5228456251405,29.328716079953,19.));
#8238=CARTESIAN_POINT('',(-26.5228456251405,29.328716079953,18.5));
#8239=CARTESIAN_POINT('',(-26.5228456251405,29.328716079953,19.));
#8240=CARTESIAN_POINT('',(-21.4468059458827,29.9006826149846,18.5));
#8241=CARTESIAN_POINT('Origin',(-26.4108745336824,28.3350046154535,19.));
#8242=CARTESIAN_POINT('',(-27.1161971101824,29.0438911106552,18.5));
#8243=CARTESIAN_POINT('',(-27.1161971101824,29.0438911106552,19.));
#8244=CARTESIAN_POINT('Origin',(-26.4108745336824,28.3350046154535,18.5));
#8245=CARTESIAN_POINT('Origin',(-29.2414240245077,26.9293487501995,19.));
#8246=CARTESIAN_POINT('',(-29.2414240245077,26.9293487501995,18.5));
#8247=CARTESIAN_POINT('',(-29.2414240245077,26.9293487501995,19.));
#8248=CARTESIAN_POINT('',(-26.4568269386167,29.6999463062668,18.5));
#8249=CARTESIAN_POINT('Origin',(-28.5361014480077,26.2204622549978,19.));
#8250=CARTESIAN_POINT('',(-29.5361014480077,26.2204622549978,18.5));
#8251=CARTESIAN_POINT('',(-29.5361014480077,26.2204622549978,19.));
#8252=CARTESIAN_POINT('Origin',(-28.5361014480077,26.2204622549978,18.5));
#8253=CARTESIAN_POINT('Origin',(-29.5361014480077,23.9853421961411,19.));
#8254=CARTESIAN_POINT('',(-29.5361014480077,23.9853421961411,18.5));
#8255=CARTESIAN_POINT('',(-29.5361014480077,23.9853421961411,19.));
#8256=CARTESIAN_POINT('',(-29.5361014480077,24.2177430103512,18.5));
#8257=CARTESIAN_POINT('Origin',(-28.5361014480077,23.9853421961411,19.));
#8258=CARTESIAN_POINT('',(-29.2499614098888,23.285053716425,18.5));
#8259=CARTESIAN_POINT('',(-29.2499614098888,23.285053716425,19.));
#8260=CARTESIAN_POINT('Origin',(-28.5361014480077,23.9853421961411,18.5));
#8261=CARTESIAN_POINT('Origin',(-27.2066069228731,21.2020993362501,19.));
#8262=CARTESIAN_POINT('',(-27.2066069228731,21.2020993362501,18.5));
#8263=CARTESIAN_POINT('',(-27.2066069228731,21.2020993362501,19.));
#8264=CARTESIAN_POINT('',(-25.1951014382868,19.1516111872338,18.5));
#8265=CARTESIAN_POINT('Origin',(-26.492746960992,21.9023878159662,19.));
#8266=CARTESIAN_POINT('',(-26.5560774487021,20.9043952061106,18.5));
#8267=CARTESIAN_POINT('',(-26.5560774487021,20.9043952061106,19.));
#8268=CARTESIAN_POINT('Origin',(-26.492746960992,21.9023878159662,18.5));
#8269=CARTESIAN_POINT('Origin',(-20.7477218067072,20.5358093148237,19.));
#8270=CARTESIAN_POINT('',(-20.7477218067072,20.5358093148237,18.5));
#8271=CARTESIAN_POINT('',(-20.7477218067072,20.5358093148237,19.));
#8272=CARTESIAN_POINT('',(-18.3537749038095,20.3838945376847,18.5));
#8273=CARTESIAN_POINT('Origin',(-20.652726075142,22.0327982296081,19.));
#8274=CARTESIAN_POINT('',(-20.652726075142,20.5327982296071,18.5));
#8275=CARTESIAN_POINT('',(-20.652726075142,20.5327982296071,19.));
#8276=CARTESIAN_POINT('Origin',(-20.652726075142,22.0327982296081,18.5));
#8277=CARTESIAN_POINT('Origin',(-15.1536728255497,20.5327982296071,19.));
#8278=CARTESIAN_POINT('',(-15.5478417425962,20.5327982296071,18.5));
#8279=CARTESIAN_POINT('',(-15.5478417425962,20.5327982296071,19.));
#8280=CARTESIAN_POINT('',(-15.4229125547249,20.5327982296071,18.5));
#8281=CARTESIAN_POINT('Origin',(-15.5478417425962,120.532798229607,19.));
#8282=CARTESIAN_POINT('',(-15.0632214243815,20.533972520766,18.5));
#8283=CARTESIAN_POINT('',(-15.0632214243815,20.533972520766,19.));
#8284=CARTESIAN_POINT('Origin',(-15.5478417425962,120.532798229607,18.5));
#8285=CARTESIAN_POINT('Origin',(-15.0362789163973,14.9745292642475,19.));
#8286=CARTESIAN_POINT('',(-11.0997123508774,18.9002876491226,18.5));
#8287=CARTESIAN_POINT('',(-11.0997123508774,18.9002876491226,19.));
#8288=CARTESIAN_POINT('Origin',(-15.0362789163973,14.9745292642475,18.5));
#8289=CARTESIAN_POINT('Origin',(-15.0254707357525,14.9637210836027,19.));
#8290=CARTESIAN_POINT('',(-9.46602747923395,14.9367785756188,18.5));
#8291=CARTESIAN_POINT('',(-9.46602747923395,14.9367785756188,19.));
#8292=CARTESIAN_POINT('Origin',(-15.0254707357525,14.9637210836027,18.5));
#8293=CARTESIAN_POINT('Origin',(-15.6921522839002,24.4501438245613,8.6));
#8294=CARTESIAN_POINT('',(-4.88927830720691,1.65310616413992,8.6));
#8295=CARTESIAN_POINT('Origin',(-4.88927830720691,5.31072169279307,8.6));
#8296=CARTESIAN_POINT('',(-28.3468938358601,25.1107216927931,8.6));
#8297=CARTESIAN_POINT('Origin',(-24.6892783072069,25.1107216927931,8.6));
#8298=CARTESIAN_POINT('',(-4.89952178519528,17.3545161944422,8.6));
#8299=CARTESIAN_POINT('Origin',(-4.89952178519528,19.1340879581285,8.6));
#8300=CARTESIAN_POINT('',(-20.5154838055578,25.1004782148047,8.6));
#8301=CARTESIAN_POINT('Origin',(-18.7359120418715,25.1004782148047,8.6));
#8302=CARTESIAN_POINT('',(-8.54689383586007,25.1107216927931,8.6));
#8303=CARTESIAN_POINT('Origin',(-4.88927830720691,25.1107216927931,8.6));
#8304=CARTESIAN_POINT('Origin',(-15.0362789163973,14.9745292642475,18.75));
#8305=CARTESIAN_POINT('',(-10.7461586529797,19.2538413454045,19.));
#8306=CARTESIAN_POINT('Ctrl Pts',(-11.0997123508774,18.9002876491226,18.5));
#8307=CARTESIAN_POINT('Ctrl Pts',(-11.0702462030105,18.9297471128432,18.5416666666667));
#8308=CARTESIAN_POINT('Ctrl Pts',(-11.0407808900234,18.9592074126868,18.5833333333333));
#8309=CARTESIAN_POINT('Ctrl Pts',(-10.9818519338798,19.0181296845492,18.6666666666667));
#8310=CARTESIAN_POINT('Ctrl Pts',(-10.9523882907234,19.047591656568,18.7083333333333));
#8311=CARTESIAN_POINT('Ctrl Pts',(-10.8934626743122,19.1065172727097,18.7916666666667));
#8312=CARTESIAN_POINT('Ctrl Pts',(-10.8640007010576,19.1359809168326,18.8333333333333));
#8313=CARTESIAN_POINT('Ctrl Pts',(-10.8050784245212,19.1949098771114,18.9166666666667));
#8314=CARTESIAN_POINT('Ctrl Pts',(-10.7756181212394,19.2243751932674,18.9583333333333));
#8315=CARTESIAN_POINT('Ctrl Pts',(-10.7461586529797,19.2538413454045,19.));
#8316=CARTESIAN_POINT('',(-15.0656445259725,21.0339666493102,19.));
#8317=CARTESIAN_POINT('Origin',(-15.0362789163973,14.9745292642475,19.));
#8318=CARTESIAN_POINT('',(-15.0656445259725,21.0339666493102,19.));
#8319=CARTESIAN_POINT('Origin',(-15.5478417425962,120.532798229607,18.75));
#8320=CARTESIAN_POINT('',(-15.5478417425962,21.0327982296071,19.));
#8321=CARTESIAN_POINT('',(-15.5478417425962,21.0327982296071,19.));
#8322=CARTESIAN_POINT('Origin',(-15.5478417425962,120.532798229607,19.));
#8323=CARTESIAN_POINT('Origin',(-15.4229125547249,20.7827982296071,18.75));
#8324=CARTESIAN_POINT('',(-20.652726075142,21.0327982296071,19.));
#8325=CARTESIAN_POINT('',(-20.652726075142,21.0327982296071,19.));
#8326=CARTESIAN_POINT('',(-15.4229125547249,21.0327982296071,19.));
#8327=CARTESIAN_POINT('Origin',(-20.652726075142,22.0327982296081,18.75));
#8328=CARTESIAN_POINT('',(-20.7160565628522,21.0348056197515,19.));
#8329=CARTESIAN_POINT('',(-20.7160565628522,21.0348056197515,19.));
#8330=CARTESIAN_POINT('Origin',(-20.652726075142,22.0327982296081,19.));
#8331=CARTESIAN_POINT('Origin',(-18.337942281882,20.6333926901486,18.75));
#8332=CARTESIAN_POINT('',(-26.5244122048471,21.4033915110384,19.));
#8333=CARTESIAN_POINT('',(-18.3221096599545,20.8828908426125,19.));
#8334=CARTESIAN_POINT('',(-26.5244122048471,21.4033915110384,19.));
#8335=CARTESIAN_POINT('Origin',(-26.492746960992,21.9023878159662,18.75));
#8336=CARTESIAN_POINT('',(-26.8496769419326,21.5522435761082,19.));
#8337=CARTESIAN_POINT('',(-26.8496769419326,21.5522435761082,19.));
#8338=CARTESIAN_POINT('Origin',(-26.492746960992,21.9023878159662,19.));
#8339=CARTESIAN_POINT('Origin',(-25.0166364478165,19.3266833071628,18.75));
#8340=CARTESIAN_POINT('',(-28.8930314289483,23.6351979562831,19.));
#8341=CARTESIAN_POINT('',(-24.8381714573462,19.5017554270918,19.));
#8342=CARTESIAN_POINT('',(-28.8930314289483,23.6351979562831,19.));
#8343=CARTESIAN_POINT('Origin',(-28.5361014480077,23.9853421961411,18.75));
#8344=CARTESIAN_POINT('',(-29.0361014480077,23.9853421961411,19.));
#8345=CARTESIAN_POINT('',(-29.0361014480077,23.9853421961411,19.));
#8346=CARTESIAN_POINT('Origin',(-28.5361014480077,23.9853421961411,19.));
#8347=CARTESIAN_POINT('Origin',(-29.2861014480077,24.2177430103512,18.75));
#8348=CARTESIAN_POINT('',(-29.0361014480077,26.2204622549978,19.));
#8349=CARTESIAN_POINT('',(-29.0361014480077,24.2177430103512,19.));
#8350=CARTESIAN_POINT('',(-29.0361014480077,26.2204622549978,19.));
#8351=CARTESIAN_POINT('Origin',(-28.5361014480077,26.2204622549978,18.75));
#8352=CARTESIAN_POINT('',(-28.8887627362577,26.5749055025986,19.));
#8353=CARTESIAN_POINT('',(-28.8887627362577,26.5749055025986,19.));
#8354=CARTESIAN_POINT('Origin',(-28.5361014480077,26.2204622549978,19.));
#8355=CARTESIAN_POINT('Origin',(-26.2804962944917,29.5227246824664,18.75));
#8356=CARTESIAN_POINT('',(-26.7635358219324,28.6894478630543,19.));
#8357=CARTESIAN_POINT('',(-26.1041656503667,29.345503058666,19.));
#8358=CARTESIAN_POINT('',(-26.7635358219324,28.6894478630543,19.));
#8359=CARTESIAN_POINT('Origin',(-26.4108745336824,28.3350046154535,18.75));
#8360=CARTESIAN_POINT('',(-26.4668600794115,28.8318603477032,19.));
#8361=CARTESIAN_POINT('',(-26.4668600794115,28.8318603477032,19.));
#8362=CARTESIAN_POINT('Origin',(-26.4108745336824,28.3350046154535,19.));
#8363=CARTESIAN_POINT('Origin',(-21.4188131730182,29.6522547488597,18.75));
#8364=CARTESIAN_POINT('',(-20.5931204026082,29.4937114644995,19.));
#8365=CARTESIAN_POINT('',(-21.3908204001537,29.4038268827348,19.));
#8366=CARTESIAN_POINT('',(-20.5931204026082,29.4937114644995,19.));
#8367=CARTESIAN_POINT('Origin',(-20.4811493111501,28.4999999999997,18.75));
#8368=CARTESIAN_POINT('',(-20.4811493111501,29.5,19.));
#8369=CARTESIAN_POINT('',(-20.4811493111501,29.5,19.));
#8370=CARTESIAN_POINT('Origin',(-20.4811493111501,28.4999999999997,19.));
#8371=CARTESIAN_POINT('Origin',(-18.0866507975252,29.75,18.75));
#8372=CARTESIAN_POINT('',(-9.51998202325534,29.5,19.));
#8373=CARTESIAN_POINT('',(-9.51998202325534,29.5,19.));
#8374=CARTESIAN_POINT('',(-18.0866507975252,29.5,19.));
#8375=CARTESIAN_POINT('Origin',(-9.51998202325534,28.4999999999996,18.75));
#8376=CARTESIAN_POINT('',(-9.39832182610329,29.4925718092052,19.));
#8377=CARTESIAN_POINT('',(-9.39832182610329,29.4925718092052,19.));
#8378=CARTESIAN_POINT('Origin',(-9.51998202325534,28.4999999999996,19.));
#8379=CARTESIAN_POINT('Origin',(-12.1637909407195,30.0834081721396,18.75));
#8380=CARTESIAN_POINT('',(-4.42688077355167,28.8832189211081,19.));
#8381=CARTESIAN_POINT('',(-4.42688077355167,28.8832189211081,19.));
#8382=CARTESIAN_POINT('',(-12.1942059900075,29.8352652198383,19.));
#8383=CARTESIAN_POINT('Origin',(-4.88927830720691,25.1107216927931,18.75));
#8384=CARTESIAN_POINT('',(-1.11678107889194,25.5731192264483,19.));
#8385=CARTESIAN_POINT('',(-0.620495174289325,25.6339493250243,18.5));
#8386=CARTESIAN_POINT('',(-1.11678107889194,25.5731192264483,19.));
#8387=CARTESIAN_POINT('Origin',(-4.88927830720691,25.1107216927931,18.5));
#8388=CARTESIAN_POINT('Origin',(-4.88927830720691,25.1107216927931,19.));
#8389=CARTESIAN_POINT('Origin',(-0.604024921256996,23.4446720175285,18.75));
#8390=CARTESIAN_POINT('',(-0.507428190794773,20.6016781738967,19.));
#8391=CARTESIAN_POINT('',(-0.852167873558302,23.4142569682405,19.));
#8392=CARTESIAN_POINT('',(-0.011142286192162,20.6625082724727,18.5));
#8393=CARTESIAN_POINT('',(-0.507428190794773,20.6016781738967,19.));
#8394=CARTESIAN_POINT('',(-0.355881968955691,23.4750870668165,18.5));
#8395=CARTESIAN_POINT('Origin',(-1.50000000000038,20.4800179767447,18.75));
#8396=CARTESIAN_POINT('',(-0.499999999999998,20.4800179767447,19.));
#8397=CARTESIAN_POINT('Origin',(-1.50000000000038,20.4800179767447,19.));
#8398=CARTESIAN_POINT('',(2.11386064724713E-15,20.4800179767447,18.5));
#8399=CARTESIAN_POINT('',(-0.499999999999998,20.4800179767447,19.));
#8400=CARTESIAN_POINT('Origin',(-1.50000000000038,20.4800179767447,18.5));
#8401=CARTESIAN_POINT('Origin',(-0.249999999999997,16.9844972567056,18.75));
#8402=CARTESIAN_POINT('',(-0.499999999999995,9.51885068884984,19.));
#8403=CARTESIAN_POINT('',(-0.499999999999997,16.9844972567056,19.));
#8404=CARTESIAN_POINT('',(4.4067824247818E-15,9.51885068884984,18.5));
#8405=CARTESIAN_POINT('',(-0.499999999999995,9.51885068884984,19.));
#8406=CARTESIAN_POINT('',(2.84494650060196E-15,16.9844972567056,18.5));
#8407=CARTESIAN_POINT('Origin',(-1.50000000000024,9.51885068884986,18.75));
#8408=CARTESIAN_POINT('',(-0.506288535500522,9.40687959739178,19.));
#8409=CARTESIAN_POINT('Origin',(-1.50000000000024,9.51885068884986,19.));
#8410=CARTESIAN_POINT('',(-0.00943280325078496,9.35089405166275,18.5));
#8411=CARTESIAN_POINT('',(-0.506288535500522,9.40687959739178,19.));
#8412=CARTESIAN_POINT('Origin',(-1.50000000000024,9.51885068884986,18.5));
#8413=CARTESIAN_POINT('Origin',(0.152926315598855,13.0245040201872,18.75));
#8414=CARTESIAN_POINT('',(-1.16813965229678,3.53313992058853,19.));
#8415=CARTESIAN_POINT('',(-0.671283920047039,3.4771543748595,18.5));
#8416=CARTESIAN_POINT('',(-1.16813965229678,3.53313992058853,19.));
#8417=CARTESIAN_POINT('',(0.401354181723723,12.9965112473227,18.5));
#8418=CARTESIAN_POINT('',(-0.0955015505260137,13.0524967930517,19.));
#8419=CARTESIAN_POINT('Origin',(-1.66499538454653,3.58912546631758,18.75));
#8420=CARTESIAN_POINT('',(-1.31055213694565,3.23646417806756,19.));
#8421=CARTESIAN_POINT('Origin',(-1.66499538454653,3.58912546631758,19.));
#8422=CARTESIAN_POINT('',(-0.956108889344776,2.88380288981757,18.5));
#8423=CARTESIAN_POINT('',(-1.31055213694565,3.23646417806756,19.));
#8424=CARTESIAN_POINT('Origin',(-1.66499538454653,3.58912546631758,18.5));
#8425=CARTESIAN_POINT('Origin',(-0.464527910187313,3.73231552412536,18.75));
#8426=CARTESIAN_POINT('',(-3.42509449740134,1.11123726374228,19.));
#8427=CARTESIAN_POINT('',(-3.07065124980047,0.758575975492288,18.5));
#8428=CARTESIAN_POINT('',(-3.42509449740134,1.11123726374228,19.));
#8429=CARTESIAN_POINT('',(-0.28730628638688,3.55598488000036,18.5));
#8430=CARTESIAN_POINT('',(-0.641749533987747,3.90864616825036,19.));
#8431=CARTESIAN_POINT('Origin',(-3.77953774500221,1.46389855199228,18.75));
#8432=CARTESIAN_POINT('',(-3.77953774500221,0.96389855199229,19.));
#8433=CARTESIAN_POINT('Origin',(-3.77953774500221,1.46389855199228,19.));
#8434=CARTESIAN_POINT('',(-3.77953774500221,0.463898551992288,18.5));
#8435=CARTESIAN_POINT('',(-3.77953774500221,0.96389855199229,19.));
#8436=CARTESIAN_POINT('Origin',(-3.77953774500221,1.46389855199228,18.5));
#8437=CARTESIAN_POINT('Origin',(-10.8534050438796,0.713898551992287,18.75));
#8438=CARTESIAN_POINT('',(-6.01465780385888,0.963898551992286,19.));
#8439=CARTESIAN_POINT('',(-6.01465780385888,0.463898551992288,18.5));
#8440=CARTESIAN_POINT('',(-6.01465780385888,0.963898551992286,19.));
#8441=CARTESIAN_POINT('',(-10.8534050438796,0.463898551992288,18.5));
#8442=CARTESIAN_POINT('',(-10.8534050438796,0.963898551992286,19.));
#8443=CARTESIAN_POINT('Origin',(-6.01465780385887,1.4638985519923,18.75));
#8444=CARTESIAN_POINT('',(-6.36480204371692,1.10696857105173,19.));
#8445=CARTESIAN_POINT('Origin',(-6.01465780385887,1.4638985519923,19.));
#8446=CARTESIAN_POINT('',(-6.71494628357496,0.750038590111157,18.5));
#8447=CARTESIAN_POINT('',(-6.36480204371692,1.10696857105173,19.));
#8448=CARTESIAN_POINT('Origin',(-6.01465780385887,1.4638985519923,18.5));
#8449=CARTESIAN_POINT('Origin',(-15.7926606978681,10.0053816255599,18.75));
#8450=CARTESIAN_POINT('',(-8.44775642389183,3.15032305806741,19.));
#8451=CARTESIAN_POINT('',(-8.79790066374987,2.79339307712685,18.5));
#8452=CARTESIAN_POINT('',(-8.44775642389183,3.15032305806741,19.));
#8453=CARTESIAN_POINT('',(-15.9677328177972,9.82691663508957,18.5));
#8454=CARTESIAN_POINT('',(-15.6175885779391,10.1838466160301,19.));
#8455=CARTESIAN_POINT('Origin',(-8.09761218403378,3.50725303900799,18.75));
#8456=CARTESIAN_POINT('',(-8.5966084889616,3.47558779515293,19.));
#8457=CARTESIAN_POINT('Origin',(-8.09761218403378,3.50725303900799,19.));
#8458=CARTESIAN_POINT('',(-9.0956047938894,3.44392255129788,18.5));
#8459=CARTESIAN_POINT('',(-8.5966084889616,3.47558779515293,19.));
#8460=CARTESIAN_POINT('Origin',(-8.09761218403378,3.50725303900799,18.5));
#8461=CARTESIAN_POINT('Origin',(-9.70746000988541,17.0333802514339,18.75));
#8462=CARTESIAN_POINT('',(-8.96519438024848,9.28394343714786,19.));
#8463=CARTESIAN_POINT('',(-9.46419068517628,9.2522781932928,18.5));
#8464=CARTESIAN_POINT('',(-8.96519438024848,9.28394343714786,19.));
#8465=CARTESIAN_POINT('',(-9.95695816234931,17.0175476295063,18.5));
#8466=CARTESIAN_POINT('',(-9.45796185742151,17.0492128733614,19.));
#8467=CARTESIAN_POINT('Origin',(-7.9672017703919,9.34727392485799,18.75));
#8468=CARTESIAN_POINT('',(-8.96720177039288,9.34727392485798,19.));
#8469=CARTESIAN_POINT('Origin',(-7.9672017703919,9.34727392485799,19.));
#8470=CARTESIAN_POINT('',(-9.46720177039288,9.34727392485798,18.5));
#8471=CARTESIAN_POINT('',(-8.96720177039288,9.34727392485798,19.));
#8472=CARTESIAN_POINT('Origin',(-7.9672017703919,9.34727392485799,18.5));
#8473=CARTESIAN_POINT('Origin',(-9.21720177039288,19.6482354995058,18.75));
#8474=CARTESIAN_POINT('',(-8.96720177039288,14.4521582574094,19.));
#8475=CARTESIAN_POINT('',(-8.96720177039288,19.6482354995058,19.));
#8476=CARTESIAN_POINT('',(-9.46720177039287,14.4521582574094,18.5));
#8477=CARTESIAN_POINT('',(-8.96720177039288,14.4521582574094,19.));
#8478=CARTESIAN_POINT('',(-9.46720177039288,19.6482354995058,18.5));
#8479=CARTESIAN_POINT('Origin',(90.5327982296072,14.4521582574094,18.75));
#8480=CARTESIAN_POINT('',(-8.96603335068974,14.9343554740278,19.));
#8481=CARTESIAN_POINT('',(-8.96603335068974,14.9343554740278,19.));
#8482=CARTESIAN_POINT('Origin',(90.5327982296072,14.4521582574094,18.5));
#8483=CARTESIAN_POINT('Origin',(90.5327982296072,14.4521582574094,19.));
#8484=CARTESIAN_POINT('Origin',(-15.0254707357525,14.9637210836027,18.75));
#8485=CARTESIAN_POINT('Origin',(-15.0254707357525,14.9637210836027,19.));
#8486=CARTESIAN_POINT('Origin',(-0.011142286192162,20.6625082724727,19.));
#8487=CARTESIAN_POINT('',(-0.620495174289325,25.6339493250243,19.));
#8488=CARTESIAN_POINT('',(-0.011142286192162,20.6625082724727,19.));
#8489=CARTESIAN_POINT('Origin',(-1.50000000000038,20.4800179767447,19.));
#8490=CARTESIAN_POINT('',(2.11386064724713E-15,20.4800179767447,19.));
#8491=CARTESIAN_POINT('Origin',(4.53905508982503E-15,9.51885068884985,19.));
#8492=CARTESIAN_POINT('',(4.4067824247818E-15,9.51885068884984,19.));
#8493=CARTESIAN_POINT('Origin',(-1.50000000000024,9.51885068884986,19.));
#8494=CARTESIAN_POINT('',(-0.00943280325078496,9.35089405166275,19.));
#8495=CARTESIAN_POINT('Origin',(-0.671283920047039,3.4771543748595,19.));
#8496=CARTESIAN_POINT('',(-0.671283920047039,3.4771543748595,19.));
#8497=CARTESIAN_POINT('Origin',(-1.66499538454653,3.58912546631758,19.));
#8498=CARTESIAN_POINT('',(-0.956108889344776,2.88380288981757,19.));
#8499=CARTESIAN_POINT('Origin',(-3.07065124980047,0.758575975492288,19.));
#8500=CARTESIAN_POINT('',(-3.07065124980047,0.758575975492288,19.));
#8501=CARTESIAN_POINT('Origin',(-3.77953774500221,1.46389855199228,19.));
#8502=CARTESIAN_POINT('',(-3.77953774500221,0.463898551992288,19.));
#8503=CARTESIAN_POINT('Origin',(-6.01465780385888,0.463898551992288,19.));
#8504=CARTESIAN_POINT('',(-6.01465780385888,0.463898551992288,19.));
#8505=CARTESIAN_POINT('Origin',(-6.01465780385887,1.4638985519923,19.));
#8506=CARTESIAN_POINT('',(-6.71494628357496,0.750038590111157,19.));
#8507=CARTESIAN_POINT('Origin',(-8.79790066374987,2.79339307712685,19.));
#8508=CARTESIAN_POINT('',(-8.79790066374987,2.79339307712685,19.));
#8509=CARTESIAN_POINT('Origin',(-8.09761218403378,3.50725303900799,19.));
#8510=CARTESIAN_POINT('',(-9.0956047938894,3.44392255129788,19.));
#8511=CARTESIAN_POINT('Origin',(-9.46419068517628,9.2522781932928,19.));
#8512=CARTESIAN_POINT('',(-9.46419068517628,9.2522781932928,19.));
#8513=CARTESIAN_POINT('Origin',(-7.9672017703919,9.34727392485799,19.));
#8514=CARTESIAN_POINT('',(-9.46720177039288,9.34727392485798,19.));
#8515=CARTESIAN_POINT('Origin',(-9.46720177039288,14.8463271744503,19.));
#8516=CARTESIAN_POINT('',(-9.46720177039287,14.4521582574094,19.));
#8517=CARTESIAN_POINT('Origin',(90.5327982296072,14.4521582574094,19.));
#8518=CARTESIAN_POINT('Origin',(-15.6921522839002,24.4501438245613,19.));
#8519=CARTESIAN_POINT('',(-27.8468938358601,25.1107216927931,19.));
#8520=CARTESIAN_POINT('Origin',(-24.6892783072069,25.1107216927931,19.));
#8521=CARTESIAN_POINT('',(-4.88927830720691,2.15310616413992,19.));
#8522=CARTESIAN_POINT('Origin',(-4.88927830720691,5.31072169279308,19.));
#8523=CARTESIAN_POINT('',(-8.04689383586007,25.1107216927931,19.));
#8524=CARTESIAN_POINT('Origin',(-4.88927830720691,25.1107216927931,19.));
#8525=CARTESIAN_POINT('Origin',(-4.89952178519528,19.1640879581285,16.5));
#8526=CARTESIAN_POINT('',(-4.89952178519528,17.3545161944422,16.5));
#8527=CARTESIAN_POINT('Origin',(-4.89952178519528,19.1340879581285,16.5));
#8528=CARTESIAN_POINT('Origin',(-10.8359120418715,25.1004782148047,16.5));
#8529=CARTESIAN_POINT('Origin',(-4.89952178519528,11.2640879581285,16.5));
#8530=CARTESIAN_POINT('Origin',(-18.7359120418715,25.1004782148047,16.5));
#8531=CARTESIAN_POINT('',(-20.5154838055578,25.1004782148047,16.5));
#8532=CARTESIAN_POINT('Origin',(-18.7359120418715,25.1004782148047,16.5));
#8533=CARTESIAN_POINT('Origin',(-4.88927830720691,5.31072169279307,8.85));
#8534=CARTESIAN_POINT('',(-4.88927830720691,2.15310616413992,9.1));
#8535=CARTESIAN_POINT('Origin',(-4.88927830720691,5.31072169279307,9.1));
#8536=CARTESIAN_POINT('',(-4.88927830720691,1.90310616413992,8.85));
#8537=CARTESIAN_POINT('Origin',(-4.88927830720691,5.31072169279308,19.));
#8538=CARTESIAN_POINT('',(-4.88927830720691,2.15310616413992,19.));
#8539=CARTESIAN_POINT('Origin',(-4.88927830720691,25.1107216927931,8.85));
#8540=CARTESIAN_POINT('',(-8.04689383586007,25.1107216927931,9.1));
#8541=CARTESIAN_POINT('Origin',(-4.88927830720691,25.1107216927931,9.1));
#8542=CARTESIAN_POINT('',(-8.29689383586007,25.1107216927931,8.85));
#8543=CARTESIAN_POINT('Origin',(-4.88927830720691,25.1107216927931,19.));
#8544=CARTESIAN_POINT('',(-8.04689383586007,25.1107216927931,19.));
#8545=CARTESIAN_POINT('Origin',(-24.6892783072069,25.1107216927931,8.85));
#8546=CARTESIAN_POINT('',(-27.8468938358601,25.1107216927931,9.1));
#8547=CARTESIAN_POINT('',(-28.0968938358601,25.1107216927931,8.85));
#8548=CARTESIAN_POINT('Origin',(-24.6892783072069,25.1107216927931,9.1));
#8549=CARTESIAN_POINT('Origin',(-24.6892783072069,25.1107216927931,19.));
#8550=CARTESIAN_POINT('',(-27.8468938358601,25.1107216927931,19.));
#8551=CARTESIAN_POINT('Origin',(-4.89952178519528,19.1340879581285,19.));
#8552=CARTESIAN_POINT('',(-4.89952178519528,17.3545161944422,19.));
#8553=CARTESIAN_POINT('Origin',(-18.7359120418715,25.1004782148047,19.));
#8554=CARTESIAN_POINT('',(-20.5154838055578,25.1004782148047,19.));
#8555=CARTESIAN_POINT('Origin',(-4.88927830720691,25.1107216927931,19.));
#11357=UNCERTAINTY_MEASURE_WITH_UNIT(LENGTH_MEASURE(0.01),#11386,
'DISTANCE_ACCURACY_VALUE',
'Maximum model space distance between geometric entities at asserted c
onnectivities');
#11370=UNCERTAINTY_MEASURE_WITH_UNIT(LENGTH_MEASURE(0.01),#11386,
'DISTANCE_ACCURACY_VALUE',
'Maximum model space distance between geometric entities at asserted c
onnectivities');
#11372=(
GEOMETRIC_REPRESENTATION_CONTEXT(3)
GLOBAL_UNCERTAINTY_ASSIGNED_CONTEXT((#11357))
GLOBAL_UNIT_ASSIGNED_CONTEXT((#11386,#11388,#11389))
REPRESENTATION_CONTEXT('','3D')
);
#11385=(
GEOMETRIC_REPRESENTATION_CONTEXT(3)
GLOBAL_UNCERTAINTY_ASSIGNED_CONTEXT((#11370))
GLOBAL_UNIT_ASSIGNED_CONTEXT((#11386,#11388,#11389))
REPRESENTATION_CONTEXT('','3D')
);
#11386=(
LENGTH_UNIT()
NAMED_UNIT(*)
SI_UNIT(.MILLI.,.METRE.)
);
#11388=(
NAMED_UNIT(*)
PLANE_ANGLE_UNIT()
SI_UNIT($,.RADIAN.)
);
#11389=(
NAMED_UNIT(*)
SI_UNIT($,.STERADIAN.)
SOLID_ANGLE_UNIT()
);
#11391=SHAPE_DEFINITION_REPRESENTATION(#11405,#11432);
#11405=PRODUCT_DEFINITION_SHAPE('',$,#11447);
#11432=SHAPE_REPRESENTATION('',(#5500),#11372);
#11445=PRODUCT_DEFINITION_CONTEXT('part definition',#11489,'design');
#11447=PRODUCT_DEFINITION('Top_Block','Top_Block',#11461,#11445);
#11461=PRODUCT_DEFINITION_FORMATION('',$,#11492);
#11489=APPLICATION_CONTEXT(
'Core Data for Automotive Mechanical Design Process');
#11490=PRODUCT_CONTEXT('part definition',#11489,'mechanical');
#11492=PRODUCT('Top_Block','Top_Block',$,(#11490));
#11540=COLOUR_RGB('Dark Blue',0.08,0.2,0.34);
#11541=FILL_AREA_STYLE_COLOUR('',#11540);
#11542=FILL_AREA_STYLE('',(#11541));
#11543=SURFACE_STYLE_FILL_AREA(#11542);
#11544=SURFACE_SIDE_STYLE('',(#11543));
#11545=SURFACE_STYLE_USAGE(.BOTH.,#11544);
#11546=PRESENTATION_STYLE_ASSIGNMENT((#11545));
ENDSEC;
END-ISO-10303-21;
